ISO-10303-21;
HEADER;
FILE_DESCRIPTION((''),'2;1');
FILE_NAME('Lock_Washer.step','2026-10-09T10:33:02-07:00',(''),(''),'','','');
FILE_SCHEMA (('AUTOMOTIVE_DESIGN { 1 0 10303 214 3 1 1 }'));
ENDSEC;
DATA;
#10=MECHANICAL_DESIGN_GEOMETRIC_PRESENTATION_REPRESENTATION('',(#848),#86330);
#761=(
BOUNDED_SURFACE()
B_SPLINE_SURFACE(1,2,((#85479,#85480,#85481,#85482,#85483,#85484,#85485,
#85486,#85487,#85488,#85489,#85490,#85491,#85492,#85493,#85494,#85495),
(#85496,#85497,#85498,#85499,#85500,#85501,#85502,#85503,#85504,#85505,
#85506,#85507,#85508,#85509,#85510,#85511,#85512)),.UNSPECIFIED.,.F.,.F.,
 .F.)
B_SPLINE_SURFACE_WITH_KNOTS((2,2),(3,2,2,2,2,2,2,2,3),(0.,1.00000000011731),
(0.,0.125,0.25,0.375,0.5,0.625,0.75,0.875,0.989797394114478),
 .UNSPECIFIED.)
GEOMETRIC_REPRESENTATION_ITEM()
RATIONAL_B_SPLINE_SURFACE(((1.,0.923879532511287,1.,0.923879532511287,1.,
0.923879532511287,1.,0.923879532511287,1.,0.923879532511287,1.,0.923879532511287,
1.,0.923879532511287,1.,0.930092549548159,0.988588189353252),(1.,0.923879532511287,
1.,0.923879532511287,1.,0.923879532511287,1.,0.923879532511287,1.,0.923879532511287,
1.,0.923879532511287,1.,0.923879532511287,1.,0.930092549548159,0.988588189353252)))
REPRESENTATION_ITEM('')
SURFACE()
) ;
#762=(
BOUNDED_SURFACE()
B_SPLINE_SURFACE(1,2,((#86143,#86144,#86145,#86146,#86147,#86148,#86149,
#86150,#86151,#86152,#86153,#86154,#86155,#86156,#86157,#86158,#86159),
(#86160,#86161,#86162,#86163,#86164,#86165,#86166,#86167,#86168,#86169,
#86170,#86171,#86172,#86173,#86174,#86175,#86176)),.UNSPECIFIED.,.F.,.F.,
 .F.)
B_SPLINE_SURFACE_WITH_KNOTS((2,2),(3,2,2,2,2,2,2,2,3),(0.,1.),(0.,0.125,
0.25,0.375,0.5,0.625,0.75,0.875,0.989795524002031),.UNSPECIFIED.)
GEOMETRIC_REPRESENTATION_ITEM()
RATIONAL_B_SPLINE_SURFACE(((1.,0.923879532511287,1.,0.923879532511287,1.,
0.923879532511287,1.,0.923879532511287,1.,0.923879532511287,1.,0.923879532511287,
1.,0.923879532511287,1.,0.930093688378829,0.988586283535283),(1.,0.923879532511287,
1.,0.923879532511287,1.,0.923879532511287,1.,0.923879532511287,1.,0.923879532511287,
1.,0.923879532511287,1.,0.923879532511287,1.,0.930093688378829,0.988586283535283)))
REPRESENTATION_ITEM('')
SURFACE()
) ;
#763=(
BOUNDED_SURFACE()
B_SPLINE_SURFACE(1,2,((#86194,#86195,#86196,#86197,#86198,#86199,#86200,
#86201,#86202,#86203,#86204,#86205,#86206,#86207,#86208,#86209,#86210,#86211,
#86212),(#86213,#86214,#86215,#86216,#86217,#86218,#86219,#86220,#86221,
#86222,#86223,#86224,#86225,#86226,#86227,#86228,#86229,#86230,#86231)),
 .UNSPECIFIED.,.F.,.F.,.F.)
B_SPLINE_SURFACE_WITH_KNOTS((2,2),(3,2,2,2,2,2,2,2,2,3),(0.,1.),(0.,0.125,
0.25,0.375,0.5,0.625,0.75,0.875,0.989795225942127,0.999693178201548),
 .UNSPECIFIED.)
GEOMETRIC_REPRESENTATION_ITEM()
RATIONAL_B_SPLINE_SURFACE(((1.,0.923879532511287,1.,0.923879532511287,1.,
0.923879532511287,1.,0.923879532511287,1.,0.923879532511287,1.,0.923879532511287,
1.,0.923879532511287,1.,0.930093869886503,0.988585979790904,0.988585979790904,
0.988585979790904),(1.,0.923879532511287,1.,0.923879532511287,1.,0.923879532511287,
1.,0.923879532511287,1.,0.923879532511287,1.,0.923879532511287,1.,0.923879532511287,
1.,0.930093869886503,0.988585979790904,0.988585979790904,0.988585979790904)))
REPRESENTATION_ITEM('')
SURFACE()
) ;
#813=(
BOUNDED_CURVE()
B_SPLINE_CURVE(2,(#86177,#86178,#86179,#86180,#86181,#86182,#86183,#86184,
#86185,#86186,#86187,#86188,#86189,#86190,#86191,#86192,#86193),
 .UNSPECIFIED.,.F.,.F.)
B_SPLINE_CURVE_WITH_KNOTS((3,2,2,2,2,2,2,2,3),(0.,0.125,0.25,0.375,0.5,
0.625,0.75,0.875,0.989794503291371),.UNSPECIFIED.)
CURVE()
GEOMETRIC_REPRESENTATION_ITEM()
RATIONAL_B_SPLINE_CURVE((1.,0.923879532511287,1.,0.923879532511287,1.,0.923879532511287,
1.,0.923879532511287,1.,0.923879532511287,1.,0.923879532511287,1.,0.923879532511287,
1.,0.93009430995461,0.988585243365237))
REPRESENTATION_ITEM('')
) ;
#824=SHAPE_REPRESENTATION_RELATIONSHIP('SRR','None',#86474,#836) ;
#836=ADVANCED_BREP_SHAPE_REPRESENTATION('',(#860),#86328) ;
#848=STYLED_ITEM('',(#86582),#860) ;
#860=MANIFOLD_SOLID_BREP('Body1',#32647) ;
#1703=B_SPLINE_CURVE_WITH_KNOTS('',3,(#85513,#85514,#85515,#85516,#85517,
#85518,#85519,#85520,#85521,#85522,#85523,#85524,#85525,#85526,#85527,#85528,
#85529,#85530,#85531,#85532,#85533,#85534,#85535,#85536,#85537,#85538,#85539,
#85540,#85541,#85542,#85543,#85544,#85545,#85546,#85547,#85548,#85549,#85550,
#85551,#85552,#85553,#85554,#85555,#85556,#85557,#85558,#85559,#85560,#85561,
#85562,#85563,#85564,#85565,#85566,#85567,#85568,#85569,#85570,#85571,#85572,
#85573,#85574,#85575,#85576,#85577,#85578,#85579,#85580,#85581,#85582,#85583,
#85584,#85585,#85586,#85587,#85588,#85589,#85590,#85591,#85592,#85593,#85594,
#85595,#85596,#85597,#85598,#85599,#85600,#85601,#85602,#85603,#85604,#85605,
#85606,#85607,#85608,#85609,#85610,#85611,#85612,#85613,#85614,#85615,#85616,
#85617,#85618,#85619,#85620,#85621,#85622,#85623,#85624,#85625,#85626,#85627,
#85628,#85629,#85630,#85631,#85632,#85633,#85634,#85635,#85636,#85637,#85638,
#85639,#85640,#85641,#85642,#85643,#85644,#85645,#85646,#85647,#85648,#85649,
#85650,#85651,#85652,#85653,#85654,#85655,#85656,#85657,#85658,#85659,#85660,
#85661,#85662,#85663,#85664,#85665,#85666,#85667,#85668,#85669,#85670,#85671,
#85672,#85673,#85674,#85675,#85676,#85677,#85678,#85679,#85680,#85681,#85682,
#85683,#85684,#85685,#85686,#85687,#85688,#85689,#85690,#85691,#85692,#85693,
#85694,#85695,#85696,#85697,#85698,#85699,#85700,#85701,#85702,#85703,#85704,
#85705,#85706,#85707,#85708,#85709,#85710,#85711,#85712,#85713,#85714,#85715,
#85716,#85717,#85718,#85719,#85720,#85721,#85722,#85723,#85724,#85725,#85726,
#85727,#85728,#85729,#85730,#85731,#85732,#85733,#85734,#85735,#85736,#85737,
#85738,#85739,#85740,#85741,#85742,#85743,#85744,#85745,#85746,#85747,#85748,
#85749,#85750,#85751,#85752,#85753),.UNSPECIFIED.,.F.,.F.,(4,3,3,3,3,3,
3,3,3,3,3,3,3,3,3,3,3,3,3,3,3,3,3,3,3,3,3,3,3,3,3,3,3,3,3,3,3,3,3,3,3,3,
3,3,3,3,3,3,3,3,3,3,3,3,3,3,3,3,3,3,3,3,3,3,3,3,3,3,3,3,3,3,3,3,3,3,3,3,
3,3,4),(0.,0.012505555813569,0.0249230581963485,0.0374326759220017,0.0497312868613704,
0.0620126665492352,0.0742948718990828,0.0869711539247056,0.0993397367790628,
0.112169868390318,0.125000000001574,0.137505555815144,0.149923058197916,
0.16243267592357,0.174731286862939,0.187012666550806,0.199294871900654,
0.211971153926278,0.224339736780635,0.237169868391891,0.250000000003148,
0.26250555581671,0.274923058199489,0.287432675925143,0.299731286864511,
0.312012666552378,0.324294871902227,0.336971153927851,0.349339736782208,
0.362169868393464,0.375000000004721,0.387505555818293,0.399923058201069,
0.412432675926722,0.42473128686609,0.437012666553957,0.449294871903807,
0.461971153929429,0.474339736783788,0.487169868395042,0.500000000006295,
0.512505555819864,0.52492305820266,0.537432675928311,0.549731286867678,
0.562012666555544,0.574294871905386,0.586971153931007,0.599339736785364,
0.612169868396617,0.625000000007869,0.63750555582144,0.64992305820421,0.662432675929864,
0.674731286869233,0.687012666557099,0.699294871906943,0.711971153932568,
0.724339736786926,0.737169868398184,0.750000000009443,0.762505555823011,
0.774923058205782,0.787432675931436,0.799731286870803,0.812012666558669,
0.824294871908519,0.836971153934144,0.849339736788504,0.862169868399761,
0.875000000011017,0.887510054669295,0.900295972101501,0.912631393721422,
0.924929982354673,0.93720989642673,0.949489203700992,0.961808005151189,
0.974159538537179,0.986588161028193,0.98979739412694),.UNSPECIFIED.) ;
#1704=B_SPLINE_CURVE_WITH_KNOTS('',3,(#85754,#85755,#85756,#85757,#85758,
#85759,#85760,#85761,#85762,#85763,#85764,#85765,#85766,#85767,#85768,#85769,
#85770,#85771,#85772,#85773,#85774,#85775,#85776,#85777,#85778,#85779,#85780,
#85781,#85782,#85783,#85784,#85785,#85786,#85787,#85788,#85789,#85790,#85791,
#85792,#85793,#85794,#85795,#85796,#85797,#85798,#85799,#85800,#85801,#85802,
#85803,#85804,#85805,#85806,#85807,#85808,#85809,#85810,#85811,#85812,#85813,
#85814,#85815,#85816,#85817,#85818,#85819,#85820,#85821,#85822,#85823,#85824,
#85825,#85826,#85827,#85828,#85829,#85830,#85831,#85832,#85833,#85834,#85835,
#85836,#85837,#85838,#85839,#85840,#85841,#85842,#85843,#85844,#85845,#85846,
#85847,#85848,#85849,#85850,#85851,#85852,#85853,#85854,#85855,#85856,#85857,
#85858,#85859,#85860,#85861,#85862,#85863,#85864,#85865,#85866,#85867,#85868,
#85869,#85870,#85871,#85872,#85873,#85874,#85875,#85876,#85877,#85878,#85879,
#85880,#85881,#85882,#85883,#85884,#85885,#85886,#85887,#85888,#85889,#85890,
#85891,#85892,#85893,#85894,#85895,#85896,#85897,#85898,#85899,#85900),
 .UNSPECIFIED.,.F.,.F.,(4,2,2,2,2,2,2,2,2,2,2,2,2,2,2,2,2,2,2,2,2,2,2,2,
2,2,2,2,2,2,2,2,2,2,2,2,2,2,2,2,2,2,2,2,2,2,2,2,2,2,2,2,2,2,2,2,2,2,2,2,
2,2,2,2,2,2,2,2,2,2,2,2,1,4),(0.,0.0143071334539869,0.028474245317343,0.0425776897392449,
0.0566436916612223,0.0706981180304496,0.0848024667917353,0.0989449686784511,
0.113213785447835,0.126288471502626,0.140595604956613,0.154762716819969,
0.168866161241871,0.18293216316385,0.196986589533071,0.211090938294356,
0.225233440181069,0.239502256950454,0.252576943005252,0.266884076459241,
0.281051188322597,0.2951546327445,0.309220634666477,0.323275061035697,0.337379409796983,
0.351521911683701,0.365790728453086,0.378865414507879,0.393172547961876,
0.407339659825232,0.421443104247129,0.435509106169106,0.449563532538323,
0.463667881299609,0.477810383186328,0.492079199955711,0.505153886010505,
0.519461019464478,0.533628131327833,0.54773157574974,0.561797577671727,
0.575852004040961,0.589956352802245,0.604098854688955,0.618367671458334,
0.631442357513131,0.645749490967132,0.659916602830487,0.674020047252389,
0.688086049174363,0.702140475543579,0.716244824304864,0.730387326191586,
0.744656142960965,0.757730829015757,0.772037962469715,0.786205074333073,
0.800308518754975,0.814374520676947,0.828428947046167,0.842533295807452,
0.85667579769416,0.870944614463543,0.884019300518384,0.898516614138413,
0.912686930054781,0.92679168641128,0.9408571728242,0.955642331987805,0.969733244122183,
0.983861047480448,0.99808103302288,0.999998904734446,1.),.UNSPECIFIED.) ;
#1705=B_SPLINE_CURVE_WITH_KNOTS('',3,(#85902,#85903,#85904,#85905,#85906,
#85907,#85908,#85909,#85910,#85911,#85912,#85913,#85914,#85915,#85916,#85917,
#85918,#85919,#85920,#85921,#85922,#85923,#85924,#85925,#85926,#85927,#85928,
#85929,#85930,#85931,#85932,#85933,#85934,#85935,#85936,#85937,#85938,#85939,
#85940,#85941,#85942,#85943,#85944,#85945,#85946,#85947,#85948,#85949,#85950,
#85951,#85952,#85953,#85954,#85955,#85956,#85957,#85958,#85959,#85960,#85961,
#85962,#85963,#85964,#85965,#85966,#85967,#85968,#85969,#85970,#85971,#85972,
#85973,#85974,#85975,#85976,#85977,#85978,#85979,#85980,#85981,#85982,#85983,
#85984,#85985,#85986,#85987,#85988,#85989,#85990,#85991,#85992,#85993,#85994,
#85995,#85996,#85997,#85998,#85999,#86000,#86001,#86002,#86003,#86004,#86005,
#86006,#86007,#86008,#86009,#86010,#86011,#86012,#86013,#86014,#86015,#86016,
#86017,#86018,#86019,#86020,#86021,#86022,#86023,#86024,#86025,#86026,#86027,
#86028,#86029,#86030,#86031,#86032,#86033,#86034,#86035,#86036,#86037,#86038,
#86039,#86040,#86041,#86042,#86043,#86044,#86045,#86046,#86047,#86048,#86049,
#86050,#86051,#86052,#86053,#86054,#86055,#86056,#86057,#86058,#86059,#86060,
#86061,#86062,#86063,#86064,#86065,#86066,#86067,#86068,#86069,#86070,#86071,
#86072,#86073,#86074,#86075,#86076,#86077,#86078,#86079,#86080,#86081,#86082,
#86083,#86084,#86085,#86086,#86087,#86088,#86089,#86090,#86091,#86092,#86093,
#86094,#86095,#86096,#86097,#86098,#86099,#86100,#86101,#86102,#86103,#86104,
#86105,#86106,#86107,#86108,#86109,#86110,#86111,#86112,#86113,#86114,#86115,
#86116,#86117,#86118,#86119,#86120,#86121,#86122,#86123,#86124,#86125,#86126,
#86127,#86128,#86129,#86130,#86131,#86132,#86133,#86134,#86135,#86136,#86137,
#86138,#86139,#86140,#86141,#86142),.UNSPECIFIED.,.F.,.F.,(4,3,3,3,3,3,
3,3,3,3,3,3,3,3,3,3,3,3,3,3,3,3,3,3,3,3,3,3,3,3,3,3,3,3,3,3,3,3,3,3,3,3,
3,3,3,3,3,3,3,3,3,3,3,3,3,3,3,3,3,3,3,3,3,3,3,3,3,3,3,3,3,3,3,3,3,3,3,3,
3,3,4),(0.,0.0126344879087828,0.0251800145560018,0.0378186062548132,0.0502440156905314,
0.0626520162199399,0.0750608509262703,0.087867825231326,0.100363927990737,
0.113326338068615,0.126288748146493,0.138923236055458,0.151468762702297,
0.164107354401133,0.176532763837236,0.188940764367353,0.201349599072213,
0.214156573377406,0.226652676136431,0.239615086214709,0.252577496292986,
0.265211984200475,0.2777575108485,0.290396102547373,0.302821511981297,0.315229512513409,
0.327638347215868,0.34044532152177,0.35294142428118,0.365903834360329,0.378866244439479,
0.391500732347696,0.404046258994235,0.416684850693202,0.429110260128054,
0.441518260657293,0.453927095363529,0.46673406966914,0.479230172428468,
0.49219258250722,0.505154992585972,0.5177894804948,0.530335007143577,0.542973598842188,
0.55539900827921,0.567807008809323,0.580215843512492,0.593022817817485,
0.605518920576294,0.618481330654379,0.631443740732464,0.644078228638788,
0.656623755284755,0.66926234698403,0.681687756419411,0.694095756948902,
0.706504591653536,0.719311565959891,0.731807668720805,0.744770078799881,
0.757732488878957,0.770366976786588,0.782912503436521,0.795551095135137,
0.807976504570989,0.820384505101515,0.832793339806436,0.84560031411119,
0.8580964168697,0.871058826947575,0.88402123702545,0.896661248545381,0.909182555765295,
0.921646976956805,0.934073048117458,0.946479128094685,0.959048489802928,
0.971489276870397,0.984122925899028,0.996756574927659,1.),.UNSPECIFIED.) ;
#2266=PLANE('',#36483) ;
#2267=PLANE('',#36484) ;
#4146=FACE_OUTER_BOUND('',#6221,.T.) ;
#4147=FACE_OUTER_BOUND('',#6222,.T.) ;
#4148=FACE_OUTER_BOUND('',#6223,.T.) ;
#4149=FACE_OUTER_BOUND('',#6224,.T.) ;
#4150=FACE_OUTER_BOUND('',#6225,.T.) ;
#4151=FACE_OUTER_BOUND('',#6226,.T.) ;
#6221=EDGE_LOOP('',(#29900,#29901,#29902,#29903)) ;
#6222=EDGE_LOOP('',(#29904,#29905,#29906,#29907)) ;
#6223=EDGE_LOOP('',(#29908,#29909,#29910,#29911)) ;
#6224=EDGE_LOOP('',(#29912,#29913,#29914,#29915)) ;
#6225=EDGE_LOOP('',(#29916,#29917,#29918,#29919)) ;
#6226=EDGE_LOOP('',(#29920,#29921,#29922,#29923)) ;
#8544=LINE('',#85464,#10863) ;
#8545=LINE('',#85466,#10864) ;
#8546=LINE('',#85468,#10865) ;
#8547=LINE('',#85469,#10866) ;
#8548=LINE('',#85473,#10867) ;
#8549=LINE('',#85475,#10868) ;
#8550=LINE('',#85477,#10869) ;
#8551=LINE('',#85478,#10870) ;
#10863=VECTOR('',#46258,10.) ;
#10864=VECTOR('',#46259,10.) ;
#10865=VECTOR('',#46260,10.) ;
#10866=VECTOR('',#46261,10.) ;
#10867=VECTOR('',#46264,10.) ;
#10868=VECTOR('',#46265,10.) ;
#10869=VECTOR('',#46266,10.) ;
#10870=VECTOR('',#46267,10.) ;
#15580=VERTEX_POINT('',#85462) ;
#15581=VERTEX_POINT('',#85463) ;
#15582=VERTEX_POINT('',#85465) ;
#15583=VERTEX_POINT('',#85467) ;
#15584=VERTEX_POINT('',#85471) ;
#15585=VERTEX_POINT('',#85472) ;
#15586=VERTEX_POINT('',#85474) ;
#15587=VERTEX_POINT('',#85476) ;
#20356=EDGE_CURVE('',#15580,#15581,#8544,.T.) ;
#20357=EDGE_CURVE('',#15581,#15582,#8545,.T.) ;
#20358=EDGE_CURVE('',#15582,#15583,#8546,.T.) ;
#20359=EDGE_CURVE('',#15583,#15580,#8547,.T.) ;
#20360=EDGE_CURVE('',#15584,#15585,#8548,.T.) ;
#20361=EDGE_CURVE('',#15585,#15586,#8549,.T.) ;
#20362=EDGE_CURVE('',#15586,#15587,#8550,.T.) ;
#20363=EDGE_CURVE('',#15587,#15584,#8551,.T.) ;
#20364=EDGE_CURVE('',#15580,#15585,#1703,.T.) ;
#20365=EDGE_CURVE('',#15581,#15584,#1704,.T.) ;
#20366=EDGE_CURVE('',#15583,#15586,#1705,.T.) ;
#20367=EDGE_CURVE('',#15582,#15587,#813,.T.) ;
#29900=ORIENTED_EDGE('',*,*,#20356,.T.) ;
#29901=ORIENTED_EDGE('',*,*,#20357,.T.) ;
#29902=ORIENTED_EDGE('',*,*,#20358,.T.) ;
#29903=ORIENTED_EDGE('',*,*,#20359,.T.) ;
#29904=ORIENTED_EDGE('',*,*,#20360,.T.) ;
#29905=ORIENTED_EDGE('',*,*,#20361,.T.) ;
#29906=ORIENTED_EDGE('',*,*,#20362,.T.) ;
#29907=ORIENTED_EDGE('',*,*,#20363,.T.) ;
#29908=ORIENTED_EDGE('',*,*,#20356,.F.) ;
#29909=ORIENTED_EDGE('',*,*,#20364,.T.) ;
#29910=ORIENTED_EDGE('',*,*,#20360,.F.) ;
#29911=ORIENTED_EDGE('',*,*,#20365,.F.) ;
#29912=ORIENTED_EDGE('',*,*,#20359,.F.) ;
#29913=ORIENTED_EDGE('',*,*,#20366,.T.) ;
#29914=ORIENTED_EDGE('',*,*,#20361,.F.) ;
#29915=ORIENTED_EDGE('',*,*,#20364,.F.) ;
#29916=ORIENTED_EDGE('',*,*,#20358,.F.) ;
#29917=ORIENTED_EDGE('',*,*,#20367,.T.) ;
#29918=ORIENTED_EDGE('',*,*,#20362,.F.) ;
#29919=ORIENTED_EDGE('',*,*,#20366,.F.) ;
#29920=ORIENTED_EDGE('',*,*,#20357,.F.) ;
#29921=ORIENTED_EDGE('',*,*,#20365,.T.) ;
#29922=ORIENTED_EDGE('',*,*,#20363,.F.) ;
#29923=ORIENTED_EDGE('',*,*,#20367,.F.) ;
#30746=CYLINDRICAL_SURFACE('',#36485,2.8) ;
#32625=ADVANCED_FACE('',(#4146),#2266,.T.) ;
#32626=ADVANCED_FACE('',(#4147),#2267,.F.) ;
#32627=ADVANCED_FACE('',(#4148),#761,.F.) ;
#32628=ADVANCED_FACE('',(#4149),#30746,.T.) ;
#32629=ADVANCED_FACE('',(#4150),#762,.F.) ;
#32630=ADVANCED_FACE('',(#4151),#763,.F.) ;
#32647=CLOSED_SHELL('',(#32625,#32626,#32627,#32628,#32629,#32630)) ;
#36482=AXIS2_PLACEMENT_3D('',#85460,#46254,#46255) ;
#36483=AXIS2_PLACEMENT_3D('',#85461,#46256,#46257) ;
#36484=AXIS2_PLACEMENT_3D('',#85470,#46262,#46263) ;
#36485=AXIS2_PLACEMENT_3D('',#85901,#46268,#46269) ;
#46254=DIRECTION('axis',(0.,0.,1.)) ;
#46255=DIRECTION('refdir',(1.,0.,0.)) ;
#46256=DIRECTION('center_axis',(1.,-1.05932475323295E-29,0.)) ;
#46257=DIRECTION('ref_axis',(0.,0.,-1.)) ;
#46258=DIRECTION('',(-1.05932475323295E-29,-1.,-1.26161707343768E-16)) ;
#46259=DIRECTION('',(0.,0.,-1.)) ;
#46260=DIRECTION('',(1.05932475323295E-29,1.,0.)) ;
#46261=DIRECTION('',(0.,0.,1.)) ;
#46262=DIRECTION('center_axis',(0.998026231470406,-0.0627984088423271,3.38208872241338E-5)) ;
#46263=DIRECTION('ref_axis',(0.0627984088782431,0.998026232041203,3.08440021028225E-21)) ;
#46264=DIRECTION('',(0.0627984089100395,0.998026232038757,-9.42827069380898E-7)) ;
#46265=DIRECTION('',(3.37541238321067E-5,-2.12403789334292E-6,-0.999999999428074)) ;
#46266=DIRECTION('',(-0.0628002171619293,-0.998026118257246,8.88096292981396E-7)) ;
#46267=DIRECTION('',(-3.37541272928291E-5,2.12398289397303E-6,0.999999999428074)) ;
#46268=DIRECTION('center_axis',(0.,0.,1.)) ;
#46269=DIRECTION('ref_axis',(-0.0314147095637551,-0.999506436208904,0.)) ;
#85460=CARTESIAN_POINT('',(0.,0.,0.)) ;
#85461=CARTESIAN_POINT('Origin',(1.4210854715202E-13,2.24999999999996,1.15)) ;
#85462=CARTESIAN_POINT('',(1.4210854715202E-13,2.79999999999996,1.15)) ;
#85463=CARTESIAN_POINT('',(1.4210854715202E-13,1.69999999999996,1.15)) ;
#85464=CARTESIAN_POINT('',(1.4210854715202E-13,2.79999999999996,1.15)) ;
#85465=CARTESIAN_POINT('',(1.4210854715202E-13,1.69999999999996,0.250000000000004)) ;
#85466=CARTESIAN_POINT('',(1.4210854715202E-13,1.69999999999996,1.15)) ;
#85467=CARTESIAN_POINT('',(1.4210854715202E-13,2.79999999999996,0.250000000000004)) ;
#85468=CARTESIAN_POINT('',(1.4210854715202E-13,1.69999999999996,0.250000000000004)) ;
#85469=CARTESIAN_POINT('',(1.4210854715202E-13,2.79999999999996,0.250000000000004)) ;
#85470=CARTESIAN_POINT('Origin',(0.124026857534672,1.97110180828134,0.15959890864801)) ;
#85471=CARTESIAN_POINT('',(0.106761092397404,1.69664435550248,0.159599907562201)) ;
#85472=CARTESIAN_POINT('',(0.175835544643537,2.7944734497289,0.159598908636084)) ;
#85473=CARTESIAN_POINT('',(0.106757295053336,1.69664459439572,0.159599945745868)) ;
#85474=CARTESIAN_POINT('',(0.175868969413493,2.7944713463616,-0.740399164074464)) ;
#85475=CARTESIAN_POINT('',(0.175835544859223,2.79447344971533,0.159598908636091)) ;
#85476=CARTESIAN_POINT('',(0.106787672964718,1.69664268279975,-0.740398325032857)) ;
#85477=CARTESIAN_POINT('',(0.17586791258293,2.79447141282259,-0.740399301632037)) ;
#85478=CARTESIAN_POINT('',(0.106787673732876,1.69664268281332,-0.740399016126806)) ;
#85479=CARTESIAN_POINT('Ctrl Pts',(1.4210854715202E-13,2.79999999999996,
1.15)) ;
#85480=CARTESIAN_POINT('Ctrl Pts',(-1.15979797464453,2.79999999999996,1.0875)) ;
#85481=CARTESIAN_POINT('Ctrl Pts',(-1.97989898732219,1.97989898732229,1.025)) ;
#85482=CARTESIAN_POINT('Ctrl Pts',(-2.79999999999986,1.15979797464463,0.962500000000004)) ;
#85483=CARTESIAN_POINT('Ctrl Pts',(-2.79999999999986,-3.53556862361244E-14,
0.900000000000004)) ;
#85484=CARTESIAN_POINT('Ctrl Pts',(-2.79999999999986,-1.15979797464471,
0.837500000000003)) ;
#85485=CARTESIAN_POINT('Ctrl Pts',(-1.97989898732219,-1.97989898732237,
0.775000000000004)) ;
#85486=CARTESIAN_POINT('Ctrl Pts',(-1.15979797464453,-2.80000000000004,
0.712500000000004)) ;
#85487=CARTESIAN_POINT('Ctrl Pts',(1.41765646048259E-13,-2.80000000000004,
0.650000000000004)) ;
#85488=CARTESIAN_POINT('Ctrl Pts',(1.15979797464481,-2.80000000000004,0.587500000000004)) ;
#85489=CARTESIAN_POINT('Ctrl Pts',(1.97989898732247,-1.97989898732237,0.525000000000004)) ;
#85490=CARTESIAN_POINT('Ctrl Pts',(2.80000000000014,-1.15979797464471,0.462500000000004)) ;
#85491=CARTESIAN_POINT('Ctrl Pts',(2.80000000000014,-3.60414884436469E-14,
0.400000000000004)) ;
#85492=CARTESIAN_POINT('Ctrl Pts',(2.80000000000014,1.15979797464463,0.337500000000003)) ;
#85493=CARTESIAN_POINT('Ctrl Pts',(1.97989898732247,1.97989898732229,0.275000000000004)) ;
#85494=CARTESIAN_POINT('Ctrl Pts',(1.23176644636502,2.72803152827974,0.217984726165415)) ;
#85495=CARTESIAN_POINT('Ctrl Pts',(0.175835544859223,2.79447344971533,0.15959890864801)) ;
#85496=CARTESIAN_POINT('Ctrl Pts',(1.4210854715202E-13,1.69999999987093,
1.15)) ;
#85497=CARTESIAN_POINT('Ctrl Pts',(-0.704163055980671,1.69999999987093,
1.0875)) ;
#85498=CARTESIAN_POINT('Ctrl Pts',(-1.20208152792574,1.20208152792585,1.025)) ;
#85499=CARTESIAN_POINT('Ctrl Pts',(-1.69999999987082,0.704163055980777,
0.962500000000004)) ;
#85500=CARTESIAN_POINT('Ctrl Pts',(-1.69999999987082,-3.54230418100854E-14,
0.900000000000004)) ;
#85501=CARTESIAN_POINT('Ctrl Pts',(-1.69999999987082,-0.704163055980848,
0.837500000000003)) ;
#85502=CARTESIAN_POINT('Ctrl Pts',(-1.20208152792574,-1.20208152792592,
0.775000000000004)) ;
#85503=CARTESIAN_POINT('Ctrl Pts',(-0.704163055980671,-1.699999999871,0.712500000000004)) ;
#85504=CARTESIAN_POINT('Ctrl Pts',(1.41900357196181E-13,-1.699999999871,
0.650000000000004)) ;
#85505=CARTESIAN_POINT('Ctrl Pts',(0.704163055980954,-1.699999999871,0.587500000000004)) ;
#85506=CARTESIAN_POINT('Ctrl Pts',(1.20208152792603,-1.20208152792592,0.525000000000004)) ;
#85507=CARTESIAN_POINT('Ctrl Pts',(1.6999999998711,-0.704163055980849,0.462500000000004)) ;
#85508=CARTESIAN_POINT('Ctrl Pts',(1.6999999998711,-3.58394217217639E-14,
0.400000000000004)) ;
#85509=CARTESIAN_POINT('Ctrl Pts',(1.6999999998711,0.704163055980777,0.337500000000003)) ;
#85510=CARTESIAN_POINT('Ctrl Pts',(1.20208152792603,1.20208152792585,0.275000000000003)) ;
#85511=CARTESIAN_POINT('Ctrl Pts',(0.747858199522055,1.65630485632982,0.217984726165415)) ;
#85512=CARTESIAN_POINT('Ctrl Pts',(0.106757295085052,1.69664459434123,0.15959890864801)) ;
#85513=CARTESIAN_POINT('Ctrl Pts',(1.4210854715202E-13,2.79999999999996,
1.15)) ;
#85514=CARTESIAN_POINT('Ctrl Pts',(-0.0714659907330142,2.79999999999996,
1.14614879098044)) ;
#85515=CARTESIAN_POINT('Ctrl Pts',(-0.143478336975935,2.797260141978,1.14220698202999)) ;
#85516=CARTESIAN_POINT('Ctrl Pts',(-0.2157221640937,2.79167762249126,1.13818924661231)) ;
#85517=CARTESIAN_POINT('Ctrl Pts',(-0.287457311955147,2.78613441033324,
1.13419980065195)) ;
#85518=CARTESIAN_POINT('Ctrl Pts',(-0.359420096621436,2.77778812917758,
1.1301355191367)) ;
#85519=CARTESIAN_POINT('Ctrl Pts',(-0.431282451398577,2.76658552138106,
1.12601289236609)) ;
#85520=CARTESIAN_POINT('Ctrl Pts',(-0.503677894492994,2.75529981055572,
1.1218596831831)) ;
#85521=CARTESIAN_POINT('Ctrl Pts',(-0.575970755478037,2.74111495138184,
1.1176472888834)) ;
#85522=CARTESIAN_POINT('Ctrl Pts',(-0.647814825571844,2.72402935956442,
1.11339433084291)) ;
#85523=CARTESIAN_POINT('Ctrl Pts',(-0.718447061165465,2.70723196007231,
1.1092131098473)) ;
#85524=CARTESIAN_POINT('Ctrl Pts',(-0.788644831515218,2.68763094901302,
1.10499272100163)) ;
#85525=CARTESIAN_POINT('Ctrl Pts',(-0.858078848064758,2.66527685062985,
1.10075203700996)) ;
#85526=CARTESIAN_POINT('Ctrl Pts',(-0.927415582489676,2.64295407196997,
1.09651729452605)) ;
#85527=CARTESIAN_POINT('Ctrl Pts',(-0.995990034381895,2.6178860276894,1.09226235220303)) ;
#85528=CARTESIAN_POINT('Ctrl Pts',(-1.06348409700904,2.59017404345893,1.0880066141315)) ;
#85529=CARTESIAN_POINT('Ctrl Pts',(-1.13098269717863,2.56246019618599,1.08375058995196)) ;
#85530=CARTESIAN_POINT('Ctrl Pts',(-1.19740013263787,2.53210230701676,1.07949380953604)) ;
#85531=CARTESIAN_POINT('Ctrl Pts',(-1.26243781057107,2.49925004240071,1.07525570443007)) ;
#85532=CARTESIAN_POINT('Ctrl Pts',(-1.32956223361152,2.4653437072116,1.07088161899123)) ;
#85533=CARTESIAN_POINT('Ctrl Pts',(-1.39521615895517,2.4287805517685,1.06652747273162)) ;
#85534=CARTESIAN_POINT('Ctrl Pts',(-1.45910321389247,2.38977358994698,1.06221399156396)) ;
#85535=CARTESIAN_POINT('Ctrl Pts',(-1.52143949914674,2.35171346804285,1.05800521417126)) ;
#85536=CARTESIAN_POINT('Ctrl Pts',(-1.58209333574021,2.31132743945059,1.05383518418228)) ;
#85537=CARTESIAN_POINT('Ctrl Pts',(-1.64082699787103,2.26885141934347,1.04972197829408)) ;
#85538=CARTESIAN_POINT('Ctrl Pts',(-1.70175237824991,2.22479035473213,1.04545528311072)) ;
#85539=CARTESIAN_POINT('Ctrl Pts',(-1.76061095855822,2.17848089233089,1.04124977763653)) ;
#85540=CARTESIAN_POINT('Ctrl Pts',(-1.81718623839383,2.13021927861696,1.03712374144037)) ;
#85541=CARTESIAN_POINT('Ctrl Pts',(-1.87376151822945,2.08195766490304,1.0329977052442)) ;
#85542=CARTESIAN_POINT('Ctrl Pts',(-1.92805331228645,2.03174466235803,1.02895116533164)) ;
#85543=CARTESIAN_POINT('Ctrl Pts',(-1.97989898732219,1.97989898732229,1.025)) ;
#85544=CARTESIAN_POINT('Ctrl Pts',(-2.03043307399382,1.92936490065066,1.02114879098044)) ;
#85545=CARTESIAN_POINT('Ctrl Pts',(-2.07941612016453,1.87650711010632,1.01720698202999)) ;
#85546=CARTESIAN_POINT('Ctrl Pts',(-2.12655278283319,1.82147557266729,1.01318924661231)) ;
#85547=CARTESIAN_POINT('Ctrl Pts',(-2.17335754942893,1.76683152025858,1.00919980065196)) ;
#85548=CARTESIAN_POINT('Ctrl Pts',(-2.21834121045665,1.71004443522516,1.00513551913671)) ;
#85549=CARTESIAN_POINT('Ctrl Pts',(-2.26123412889168,1.65130863691035,1.0010128923661)) ;
#85550=CARTESIAN_POINT('Ctrl Pts',(-2.30444523497565,1.59213712551618,0.996859683183108)) ;
#85551=CARTESIAN_POINT('Ctrl Pts',(-2.34553379709752,1.53098814317025,0.992647288883404)) ;
#85552=CARTESIAN_POINT('Ctrl Pts',(-2.38425388841422,1.46810537618418,0.988394330842914)) ;
#85553=CARTESIAN_POINT('Ctrl Pts',(-2.42232086608566,1.4062832883384,0.984213109847312)) ;
#85554=CARTESIAN_POINT('Ctrl Pts',(-2.45809817768602,1.34278596106178,0.979992721001642)) ;
#85555=CARTESIAN_POINT('Ctrl Pts',(-2.49138870707918,1.27788196256053,0.975752037009966)) ;
#85556=CARTESIAN_POINT('Ctrl Pts',(-2.52463259401104,1.21306889929801,0.971517294526055)) ;
#85557=CARTESIAN_POINT('Ctrl Pts',(-2.55539626985831,1.14685365524698,0.96726235220304)) ;
#85558=CARTESIAN_POINT('Ctrl Pts',(-2.58352644726229,1.07953281390399,0.963006614131509)) ;
#85559=CARTESIAN_POINT('Ctrl Pts',(-2.61165851582335,1.01220744666401,0.958750589951965)) ;
#85560=CARTESIAN_POINT('Ctrl Pts',(-2.63715646553154,0.943776958367677,
0.95449380953605)) ;
#85561=CARTESIAN_POINT('Ctrl Pts',(-2.65991498954339,0.874558316181138,
0.950255704430076)) ;
#85562=CARTESIAN_POINT('Ctrl Pts',(-2.68340372472112,0.803118781928595,
0.94588161899124)) ;
#85563=CARTESIAN_POINT('Ctrl Pts',(-2.70397400538774,0.730840390951192,
0.941527472731625)) ;
#85564=CARTESIAN_POINT('Ctrl Pts',(-2.72156688794646,0.658083333957503,
0.937213991563964)) ;
#85565=CARTESIAN_POINT('Ctrl Pts',(-2.73873272767254,0.587092353649035,
0.933005214171264)) ;
#85566=CARTESIAN_POINT('Ctrl Pts',(-2.75306423214998,0.515646379806024,
0.928835184182286)) ;
#85567=CARTESIAN_POINT('Ctrl Pts',(-2.76456012107105,0.444080327173848,
0.924721978294091)) ;
#85568=CARTESIAN_POINT('Ctrl Pts',(-2.77648499311034,0.369843699988586,
0.920455283110725)) ;
#85569=CARTESIAN_POINT('Ctrl Pts',(-2.78535855948034,0.295478663824547,
0.916249777636538)) ;
#85570=CARTESIAN_POINT('Ctrl Pts',(-2.79123720917151,0.221347785477126,
0.912123741440374)) ;
#85571=CARTESIAN_POINT('Ctrl Pts',(-2.79711585886268,0.147216907129704,
0.90799770524421)) ;
#85572=CARTESIAN_POINT('Ctrl Pts',(-2.79999999999986,0.0733208567859007,
0.903951165331643)) ;
#85573=CARTESIAN_POINT('Ctrl Pts',(-2.79999999999986,-3.530509218308E-14,
0.900000000000004)) ;
#85574=CARTESIAN_POINT('Ctrl Pts',(-2.79999999999986,-0.0714659907331545,
0.896148790980443)) ;
#85575=CARTESIAN_POINT('Ctrl Pts',(-2.79726014197791,-0.143478336976038,
0.89220698203)) ;
#85576=CARTESIAN_POINT('Ctrl Pts',(-2.79167762249117,-0.215722164093765,
0.88818924661232)) ;
#85577=CARTESIAN_POINT('Ctrl Pts',(-2.78613441033315,-0.287457311955207,
0.884199800651964)) ;
#85578=CARTESIAN_POINT('Ctrl Pts',(-2.77778812917749,-0.359420096621492,
0.880135519136715)) ;
#85579=CARTESIAN_POINT('Ctrl Pts',(-2.76658552138098,-0.431282451398629,
0.8760128923661)) ;
#85580=CARTESIAN_POINT('Ctrl Pts',(-2.75529981055565,-0.503677894493051,
0.871859683183112)) ;
#85581=CARTESIAN_POINT('Ctrl Pts',(-2.74111495138177,-0.575970755478099,
0.867647288883408)) ;
#85582=CARTESIAN_POINT('Ctrl Pts',(-2.72402935956434,-0.647814825571912,
0.863394330842917)) ;
#85583=CARTESIAN_POINT('Ctrl Pts',(-2.70723196007224,-0.718447061165532,
0.859213109847315)) ;
#85584=CARTESIAN_POINT('Ctrl Pts',(-2.68763094901295,-0.788644831515286,
0.854992721001645)) ;
#85585=CARTESIAN_POINT('Ctrl Pts',(-2.66527685062979,-0.858078848064827,
0.850752037009969)) ;
#85586=CARTESIAN_POINT('Ctrl Pts',(-2.64295407196991,-0.927415582489755,
0.846517294526058)) ;
#85587=CARTESIAN_POINT('Ctrl Pts',(-2.61788602768933,-0.995990034381983,
0.842262352203043)) ;
#85588=CARTESIAN_POINT('Ctrl Pts',(-2.59017404345886,-1.06348409700914,
0.838006614131511)) ;
#85589=CARTESIAN_POINT('Ctrl Pts',(-2.56246019618592,-1.13098269717874,
0.833750589951967)) ;
#85590=CARTESIAN_POINT('Ctrl Pts',(-2.53210230701669,-1.19740013263799,
0.829493809536051)) ;
#85591=CARTESIAN_POINT('Ctrl Pts',(-2.49925004240064,-1.2624378105712,0.825255704430077)) ;
#85592=CARTESIAN_POINT('Ctrl Pts',(-2.46534370721153,-1.32956223361165,
0.820881618991241)) ;
#85593=CARTESIAN_POINT('Ctrl Pts',(-2.42878055176843,-1.3952161589553,0.816527472731626)) ;
#85594=CARTESIAN_POINT('Ctrl Pts',(-2.3897735899469,-1.45910321389261,0.812213991563964)) ;
#85595=CARTESIAN_POINT('Ctrl Pts',(-2.35171346804278,-1.52143949914688,
0.808005214171265)) ;
#85596=CARTESIAN_POINT('Ctrl Pts',(-2.31132743945051,-1.58209333574035,
0.803835184182287)) ;
#85597=CARTESIAN_POINT('Ctrl Pts',(-2.2688514193434,-1.64082699787117,0.799721978294092)) ;
#85598=CARTESIAN_POINT('Ctrl Pts',(-2.22479035473205,-1.70175237825006,
0.795455283110726)) ;
#85599=CARTESIAN_POINT('Ctrl Pts',(-2.17848089233081,-1.76061095855837,
0.791249777636538)) ;
#85600=CARTESIAN_POINT('Ctrl Pts',(-2.13021927861688,-1.81718623839399,
0.787123741440374)) ;
#85601=CARTESIAN_POINT('Ctrl Pts',(-2.08195766490295,-1.87376151822962,
0.78299770524421)) ;
#85602=CARTESIAN_POINT('Ctrl Pts',(-2.03174466235794,-1.92805331228663,
0.778951165331643)) ;
#85603=CARTESIAN_POINT('Ctrl Pts',(-1.97989898732219,-1.97989898732237,
0.775000000000004)) ;
#85604=CARTESIAN_POINT('Ctrl Pts',(-1.92936490065055,-2.03043307399401,
0.771148790980441)) ;
#85605=CARTESIAN_POINT('Ctrl Pts',(-1.87650711010621,-2.07941612016473,
0.767206982029995)) ;
#85606=CARTESIAN_POINT('Ctrl Pts',(-1.82147557266717,-2.12655278283339,
0.763189246612312)) ;
#85607=CARTESIAN_POINT('Ctrl Pts',(-1.76683152025845,-2.17335754942914,
0.759199800651956)) ;
#85608=CARTESIAN_POINT('Ctrl Pts',(-1.710044435225,-2.21834121045687,0.755135519136708)) ;
#85609=CARTESIAN_POINT('Ctrl Pts',(-1.65130863691017,-2.26123412889191,
0.751012892366094)) ;
#85610=CARTESIAN_POINT('Ctrl Pts',(-1.592137125516,-2.30444523497588,0.746859683183106)) ;
#85611=CARTESIAN_POINT('Ctrl Pts',(-1.53098814317008,-2.34553379709775,
0.742647288883402)) ;
#85612=CARTESIAN_POINT('Ctrl Pts',(-1.46810537618402,-2.38425388841444,
0.738394330842911)) ;
#85613=CARTESIAN_POINT('Ctrl Pts',(-1.40628328833823,-2.42232086608588,
0.73421310984731)) ;
#85614=CARTESIAN_POINT('Ctrl Pts',(-1.34278596106162,-2.45809817768623,
0.72999272100164)) ;
#85615=CARTESIAN_POINT('Ctrl Pts',(-1.27788196256038,-2.49138870707938,
0.725752037009964)) ;
#85616=CARTESIAN_POINT('Ctrl Pts',(-1.21306889929785,-2.52463259401125,
0.721517294526053)) ;
#85617=CARTESIAN_POINT('Ctrl Pts',(-1.14685365524682,-2.55539626985851,
0.717262352203038)) ;
#85618=CARTESIAN_POINT('Ctrl Pts',(-1.07953281390383,-2.5835264472625,0.713006614131506)) ;
#85619=CARTESIAN_POINT('Ctrl Pts',(-1.01220744666384,-2.61165851582356,
0.708750589951962)) ;
#85620=CARTESIAN_POINT('Ctrl Pts',(-0.943776958367505,-2.63715646553174,
0.704493809536046)) ;
#85621=CARTESIAN_POINT('Ctrl Pts',(-0.874558316180958,-2.65991498954359,
0.700255704430072)) ;
#85622=CARTESIAN_POINT('Ctrl Pts',(-0.803118781928421,-2.68340372472132,
0.695881618991236)) ;
#85623=CARTESIAN_POINT('Ctrl Pts',(-0.730840390951022,-2.70397400538794,
0.691527472731622)) ;
#85624=CARTESIAN_POINT('Ctrl Pts',(-0.65808333395734,-2.72156688794665,
0.68721399156396)) ;
#85625=CARTESIAN_POINT('Ctrl Pts',(-0.587092353648857,-2.73873272767274,
0.68300521417126)) ;
#85626=CARTESIAN_POINT('Ctrl Pts',(-0.515646379805832,-2.75306423215018,
0.678835184182282)) ;
#85627=CARTESIAN_POINT('Ctrl Pts',(-0.444080327173642,-2.76456012107124,
0.674721978294085)) ;
#85628=CARTESIAN_POINT('Ctrl Pts',(-0.369843699988397,-2.77648499311053,
0.67045528311072)) ;
#85629=CARTESIAN_POINT('Ctrl Pts',(-0.295478663824374,-2.78535855948053,
0.666249777636534)) ;
#85630=CARTESIAN_POINT('Ctrl Pts',(-0.22134778547697,-2.7912372091717,0.662123741440371)) ;
#85631=CARTESIAN_POINT('Ctrl Pts',(-0.147216907129565,-2.79711585886286,
0.657997705244208)) ;
#85632=CARTESIAN_POINT('Ctrl Pts',(-0.0733208567857782,-2.80000000000004,
0.653951165331642)) ;
#85633=CARTESIAN_POINT('Ctrl Pts',(1.4166445794217E-13,-2.80000000000004,
0.650000000000004)) ;
#85634=CARTESIAN_POINT('Ctrl Pts',(0.071465990733294,-2.80000000000004,
0.646148790980441)) ;
#85635=CARTESIAN_POINT('Ctrl Pts',(0.143478336976213,-2.79726014197808,
0.642206982029997)) ;
#85636=CARTESIAN_POINT('Ctrl Pts',(0.215722164093974,-2.79167762249134,
0.638189246612314)) ;
#85637=CARTESIAN_POINT('Ctrl Pts',(0.287457311955519,-2.78613441033331,
0.634199800651952)) ;
#85638=CARTESIAN_POINT('Ctrl Pts',(0.359420096621906,-2.77778812917764,
0.630135519136698)) ;
#85639=CARTESIAN_POINT('Ctrl Pts',(0.431282451399145,-2.76658552138109,
0.626012892366077)) ;
#85640=CARTESIAN_POINT('Ctrl Pts',(0.503677894493549,-2.75529981055575,
0.621859683183089)) ;
#85641=CARTESIAN_POINT('Ctrl Pts',(0.575970755478578,-2.74111495138187,
0.617647288883386)) ;
#85642=CARTESIAN_POINT('Ctrl Pts',(0.647814825572372,-2.72402935956444,
0.613394330842896)) ;
#85643=CARTESIAN_POINT('Ctrl Pts',(0.718447061165981,-2.70723196007232,
0.609213109847295)) ;
#85644=CARTESIAN_POINT('Ctrl Pts',(0.788644831515725,-2.68763094901303,
0.604992721001625)) ;
#85645=CARTESIAN_POINT('Ctrl Pts',(0.858078848065254,-2.66527685062987,
0.60075203700995)) ;
#85646=CARTESIAN_POINT('Ctrl Pts',(0.927415582490178,-2.64295407196998,
0.596517294526039)) ;
#85647=CARTESIAN_POINT('Ctrl Pts',(0.995990034382399,-2.61788602768939,
0.592262352203023)) ;
#85648=CARTESIAN_POINT('Ctrl Pts',(1.06348409700955,-2.59017404345891,0.588006614131492)) ;
#85649=CARTESIAN_POINT('Ctrl Pts',(1.1309826971791,-2.56246019618599,0.583750589951951)) ;
#85650=CARTESIAN_POINT('Ctrl Pts',(1.19740013263831,-2.53210230701677,0.579493809536038)) ;
#85651=CARTESIAN_POINT('Ctrl Pts',(1.26243781057147,-2.49925004240073,0.575255704430066)) ;
#85652=CARTESIAN_POINT('Ctrl Pts',(1.32956223361191,-2.46534370721162,0.570881618991231)) ;
#85653=CARTESIAN_POINT('Ctrl Pts',(1.39521615895554,-2.42878055176853,0.566527472731617)) ;
#85654=CARTESIAN_POINT('Ctrl Pts',(1.45910321389283,-2.38977358994701,0.562213991563956)) ;
#85655=CARTESIAN_POINT('Ctrl Pts',(1.52143949914711,-2.35171346804288,0.558005214171256)) ;
#85656=CARTESIAN_POINT('Ctrl Pts',(1.58209333574058,-2.31132743945061,0.553835184182279)) ;
#85657=CARTESIAN_POINT('Ctrl Pts',(1.6408269978714,-2.26885141934349,0.549721978294083)) ;
#85658=CARTESIAN_POINT('Ctrl Pts',(1.70175237825026,-2.22479035473215,0.545455283110718)) ;
#85659=CARTESIAN_POINT('Ctrl Pts',(1.76061095855855,-2.17848089233092,0.541249777636533)) ;
#85660=CARTESIAN_POINT('Ctrl Pts',(1.81718623839415,-2.13021927861701,0.53712374144037)) ;
#85661=CARTESIAN_POINT('Ctrl Pts',(1.87376151822976,-2.08195766490309,0.532997705244207)) ;
#85662=CARTESIAN_POINT('Ctrl Pts',(1.92805331228674,-2.0317446623581,0.528951165331642)) ;
#85663=CARTESIAN_POINT('Ctrl Pts',(1.97989898732247,-1.97989898732237,0.525000000000004)) ;
#85664=CARTESIAN_POINT('Ctrl Pts',(2.03043307399411,-1.92936490065073,0.521148790980441)) ;
#85665=CARTESIAN_POINT('Ctrl Pts',(2.07941612016482,-1.87650711010639,0.517206982029996)) ;
#85666=CARTESIAN_POINT('Ctrl Pts',(2.12655278283348,-1.82147557266736,0.513189246612313)) ;
#85667=CARTESIAN_POINT('Ctrl Pts',(2.1733575494292,-1.76683152025867,0.509199800651959)) ;
#85668=CARTESIAN_POINT('Ctrl Pts',(2.21834121045691,-1.71004443522525,0.505135519136713)) ;
#85669=CARTESIAN_POINT('Ctrl Pts',(2.26123412889194,-1.65130863691045,0.501012892366101)) ;
#85670=CARTESIAN_POINT('Ctrl Pts',(2.30444523497591,-1.59213712551628,0.496859683183113)) ;
#85671=CARTESIAN_POINT('Ctrl Pts',(2.34553379709779,-1.53098814317035,0.492647288883409)) ;
#85672=CARTESIAN_POINT('Ctrl Pts',(2.38425388841448,-1.46810537618429,0.488394330842918)) ;
#85673=CARTESIAN_POINT('Ctrl Pts',(2.42232086608593,-1.4062832883385,0.484213109847316)) ;
#85674=CARTESIAN_POINT('Ctrl Pts',(2.45809817768629,-1.34278596106188,0.479992721001646)) ;
#85675=CARTESIAN_POINT('Ctrl Pts',(2.49138870707944,-1.27788196256063,0.475752037009969)) ;
#85676=CARTESIAN_POINT('Ctrl Pts',(2.52463259401131,-1.21306889929811,0.471517294526058)) ;
#85677=CARTESIAN_POINT('Ctrl Pts',(2.55539626985857,-1.14685365524709,0.467262352203043)) ;
#85678=CARTESIAN_POINT('Ctrl Pts',(2.58352644726256,-1.0795328139041,0.463006614131512)) ;
#85679=CARTESIAN_POINT('Ctrl Pts',(2.61165851582361,-1.01220744666414,0.458750589951969)) ;
#85680=CARTESIAN_POINT('Ctrl Pts',(2.63715646553179,-0.943776958367838,
0.454493809536056)) ;
#85681=CARTESIAN_POINT('Ctrl Pts',(2.65991498954363,-0.874558316181326,
0.450255704430083)) ;
#85682=CARTESIAN_POINT('Ctrl Pts',(2.68340372472137,-0.803118781928774,
0.445881618991247)) ;
#85683=CARTESIAN_POINT('Ctrl Pts',(2.70397400538799,-0.730840390951359,
0.441527472731631)) ;
#85684=CARTESIAN_POINT('Ctrl Pts',(2.72156688794672,-0.658083333957661,
0.437213991563969)) ;
#85685=CARTESIAN_POINT('Ctrl Pts',(2.73873272767281,-0.587092353649187,
0.433005214171268)) ;
#85686=CARTESIAN_POINT('Ctrl Pts',(2.75306423215025,-0.51564637980617,0.428835184182291)) ;
#85687=CARTESIAN_POINT('Ctrl Pts',(2.76456012107132,-0.444080327173988,
0.424721978294095)) ;
#85688=CARTESIAN_POINT('Ctrl Pts',(2.77648499311062,-0.369843699988715,
0.420455283110728)) ;
#85689=CARTESIAN_POINT('Ctrl Pts',(2.78535855948062,-0.295478663824664,
0.41624977763654)) ;
#85690=CARTESIAN_POINT('Ctrl Pts',(2.79123720917179,-0.221347785477232,
0.412123741440376)) ;
#85691=CARTESIAN_POINT('Ctrl Pts',(2.79711585886296,-0.147216907129799,
0.407997705244211)) ;
#85692=CARTESIAN_POINT('Ctrl Pts',(2.80000000000014,-0.0733208567859839,
0.403951165331644)) ;
#85693=CARTESIAN_POINT('Ctrl Pts',(2.80000000000014,-3.59712259978551E-14,
0.400000000000004)) ;
#85694=CARTESIAN_POINT('Ctrl Pts',(2.80000000000014,0.0714659907331161,
0.396148790980441)) ;
#85695=CARTESIAN_POINT('Ctrl Pts',(2.79726014197818,0.143478336976034,0.392206982029997)) ;
#85696=CARTESIAN_POINT('Ctrl Pts',(2.79167762249144,0.215722164093794,0.388189246612314)) ;
#85697=CARTESIAN_POINT('Ctrl Pts',(2.78613441033342,0.28745731195519,0.384199800651961)) ;
#85698=CARTESIAN_POINT('Ctrl Pts',(2.77778812917777,0.359420096621429,0.380135519136715)) ;
#85699=CARTESIAN_POINT('Ctrl Pts',(2.76658552138126,0.431282451398519,0.376012892366102)) ;
#85700=CARTESIAN_POINT('Ctrl Pts',(2.75529981055593,0.503677894492942,0.371859683183114)) ;
#85701=CARTESIAN_POINT('Ctrl Pts',(2.74111495138205,0.57597075547799,0.36764728888341)) ;
#85702=CARTESIAN_POINT('Ctrl Pts',(2.72402935956463,0.647814825571804,0.363394330842919)) ;
#85703=CARTESIAN_POINT('Ctrl Pts',(2.70723196007253,0.718447061165415,0.359213109847317)) ;
#85704=CARTESIAN_POINT('Ctrl Pts',(2.68763094901325,0.78864483151516,0.354992721001648)) ;
#85705=CARTESIAN_POINT('Ctrl Pts',(2.66527685063009,0.858078848064691,0.350752037009972)) ;
#85706=CARTESIAN_POINT('Ctrl Pts',(2.64295407197021,0.927415582489618,0.346517294526062)) ;
#85707=CARTESIAN_POINT('Ctrl Pts',(2.61788602768963,0.995990034381844,0.342262352203046)) ;
#85708=CARTESIAN_POINT('Ctrl Pts',(2.59017404345916,1.063484097009,0.338006614131515)) ;
#85709=CARTESIAN_POINT('Ctrl Pts',(2.56246019618623,1.1309826971786,0.333750589951971)) ;
#85710=CARTESIAN_POINT('Ctrl Pts',(2.532102307017,1.19740013263786,0.329493809536055)) ;
#85711=CARTESIAN_POINT('Ctrl Pts',(2.49925004240094,1.26243781057107,0.32525570443008)) ;
#85712=CARTESIAN_POINT('Ctrl Pts',(2.46534370721183,1.32956223361153,0.320881618991244)) ;
#85713=CARTESIAN_POINT('Ctrl Pts',(2.42878055176873,1.39521615895518,0.316527472731628)) ;
#85714=CARTESIAN_POINT('Ctrl Pts',(2.3897735899472,1.45910321389249,0.312213991563967)) ;
#85715=CARTESIAN_POINT('Ctrl Pts',(2.35171346804307,1.52143949914679,0.308005214171265)) ;
#85716=CARTESIAN_POINT('Ctrl Pts',(2.31132743945079,1.58209333574028,0.303835184182287)) ;
#85717=CARTESIAN_POINT('Ctrl Pts',(2.26885141934366,1.64082699787112,0.29972197829409)) ;
#85718=CARTESIAN_POINT('Ctrl Pts',(2.22479035473232,1.70175237825,0.295455283110724)) ;
#85719=CARTESIAN_POINT('Ctrl Pts',(2.17848089233108,1.76061095855831,0.291249777636537)) ;
#85720=CARTESIAN_POINT('Ctrl Pts',(2.13021927861715,1.81718623839393,0.287123741440373)) ;
#85721=CARTESIAN_POINT('Ctrl Pts',(2.08195766490322,1.87376151822955,0.282997705244209)) ;
#85722=CARTESIAN_POINT('Ctrl Pts',(2.03174466235821,1.92805331228655,0.278951165331643)) ;
#85723=CARTESIAN_POINT('Ctrl Pts',(1.97989898732247,1.97989898732229,0.275000000000004)) ;
#85724=CARTESIAN_POINT('Ctrl Pts',(1.92934672113032,2.03045125351443,0.271147405516926)) ;
#85725=CARTESIAN_POINT('Ctrl Pts',(1.87646907589625,2.07945136207899,0.267204145766144)) ;
#85726=CARTESIAN_POINT('Ctrl Pts',(1.82141617942112,2.12660365403224,0.263184910469907)) ;
#85727=CARTESIAN_POINT('Ctrl Pts',(1.76514929586526,2.17479571458848,0.259077045872825)) ;
#85728=CARTESIAN_POINT('Ctrl Pts',(1.7066101530828,2.22105676270134,0.254889835146308)) ;
#85729=CARTESIAN_POINT('Ctrl Pts',(1.64601164123507,2.26509286275836,0.250641311726231)) ;
#85730=CARTESIAN_POINT('Ctrl Pts',(1.58754824217552,2.30757740589581,0.246542479716199)) ;
#85731=CARTESIAN_POINT('Ctrl Pts',(1.5271686178725,2.34799057449375,0.24238662086617)) ;
#85732=CARTESIAN_POINT('Ctrl Pts',(1.46510735126145,2.38609732602839,0.238191623029449)) ;
#85733=CARTESIAN_POINT('Ctrl Pts',(1.40323139666294,2.42409029260176,0.234009151258246)) ;
#85734=CARTESIAN_POINT('Ctrl Pts',(1.33968428229124,2.45979009971844,0.229787809461762)) ;
#85735=CARTESIAN_POINT('Ctrl Pts',(1.27473511126994,2.49300028000314,0.225546484688788)) ;
#85736=CARTESIAN_POINT('Ctrl Pts',(1.20988456109896,2.5261600329126,0.221311600075851)) ;
#85737=CARTESIAN_POINT('Ctrl Pts',(1.14363676230229,2.55683732461154,0.217056831637654)) ;
#85738=CARTESIAN_POINT('Ctrl Pts',(1.07628859269765,2.58487966165332,0.21280158160412)) ;
#85739=CARTESIAN_POINT('Ctrl Pts',(1.00894375102516,2.61292061301535,0.208546541838861)) ;
#85740=CARTESIAN_POINT('Ctrl Pts',(0.940499272947081,2.63832660736102,0.204291060106912)) ;
#85741=CARTESIAN_POINT('Ctrl Pts',(0.871272148091887,2.66099320629711,0.200054549780001)) ;
#85742=CARTESIAN_POINT('Ctrl Pts',(0.801822366682255,2.68373270825829,0.19580441348214)) ;
#85743=CARTESIAN_POINT('Ctrl Pts',(0.731585564361363,2.7037150260078,0.19157340994441)) ;
#85744=CARTESIAN_POINT('Ctrl Pts',(0.660892332187115,2.72088612868239,0.187380560333748)) ;
#85745=CARTESIAN_POINT('Ctrl Pts',(0.590011263043028,2.73810285620388,0.183176570022037)) ;
#85746=CARTESIAN_POINT('Ctrl Pts',(0.518672017063942,2.75249343444436,0.179010972847647)) ;
#85747=CARTESIAN_POINT('Ctrl Pts',(0.447208193245961,2.76405586627579,0.17490179060408)) ;
#85748=CARTESIAN_POINT('Ctrl Pts',(0.375298345274736,2.77569046222595,0.170766961894471)) ;
#85749=CARTESIAN_POINT('Ctrl Pts',(0.303263024046943,2.78446165095677,0.166689286934451)) ;
#85750=CARTESIAN_POINT('Ctrl Pts',(0.231432282248643,2.79041916183448,0.162685441802253)) ;
#85751=CARTESIAN_POINT('Ctrl Pts',(0.212884643984362,2.7919574691657,0.161651596552725)) ;
#85752=CARTESIAN_POINT('Ctrl Pts',(0.194350566384982,2.79330843635713,0.16062266376929)) ;
#85753=CARTESIAN_POINT('Ctrl Pts',(0.175835544859223,2.79447344971533,0.15959890864801)) ;
#85754=CARTESIAN_POINT('Ctrl Pts',(1.4210854715202E-13,1.69999999999996,
1.15)) ;
#85755=CARTESIAN_POINT('Ctrl Pts',(-0.0491344664214032,1.69999999999996,
1.14563893032299)) ;
#85756=CARTESIAN_POINT('Ctrl Pts',(-0.0986947229193856,1.69786604855678,
1.14116161433639)) ;
#85757=CARTESIAN_POINT('Ctrl Pts',(-0.197622412403077,1.68919704412233,
1.13206229175992)) ;
#85758=CARTESIAN_POINT('Ctrl Pts',(-0.246986299885041,1.68270496892852,
1.12744217992741)) ;
#85759=CARTESIAN_POINT('Ctrl Pts',(-0.345200900950269,1.66532644813156,
1.11808594673948)) ;
#85760=CARTESIAN_POINT('Ctrl Pts',(-0.394052183981859,1.65445972537225,
1.1133504999456)) ;
#85761=CARTESIAN_POINT('Ctrl Pts',(-0.490749173516077,1.62839369436624,
1.10380957293898)) ;
#85762=CARTESIAN_POINT('Ctrl Pts',(-0.538596442256585,1.61320599162947,
1.09900438073851)) ;
#85763=CARTESIAN_POINT('Ctrl Pts',(-0.632803924485224,1.57863065558518,
1.08937157495477)) ;
#85764=CARTESIAN_POINT('Ctrl Pts',(-0.679164591102349,1.55924670054701,
1.08454405638323)) ;
#85765=CARTESIAN_POINT('Ctrl Pts',(-0.770056551850408,1.51642527652522,
1.07490236416373)) ;
#85766=CARTESIAN_POINT('Ctrl Pts',(-0.814580080103976,1.49297402286675,
1.07008837300884)) ;
#85767=CARTESIAN_POINT('Ctrl Pts',(-0.901240725533071,1.4423213594285,1.06053433003248)) ;
#85768=CARTESIAN_POINT('Ctrl Pts',(-0.943370504022189,1.41511051821574,
1.05579458283318)) ;
#85769=CARTESIAN_POINT('Ctrl Pts',(-1.02504405883689,1.35713483654882,1.04641395469392)) ;
#85770=CARTESIAN_POINT('Ctrl Pts',(-1.06456093267498,1.32634106753781,1.04177439801107)) ;
#85771=CARTESIAN_POINT('Ctrl Pts',(-1.13706958910421,1.26457389613212,1.03306783355715)) ;
#85772=CARTESIAN_POINT('Ctrl Pts',(-1.17033107781674,1.23383197821735,1.02898539770902)) ;
#85773=CARTESIAN_POINT('Ctrl Pts',(-1.23682484241365,1.16733821362043,1.02063893032299)) ;
#85774=CARTESIAN_POINT('Ctrl Pts',(-1.27036030432452,1.13078488863717,1.01616161433639)) ;
#85775=CARTESIAN_POINT('Ctrl Pts',(-1.33418283258382,1.0547025367344,1.00706229175992)) ;
#85776=CARTESIAN_POINT('Ctrl Pts',(-1.36449778177453,1.01520640675666,1.00244217992741)) ;
#85777=CARTESIAN_POINT('Ctrl Pts',(-1.42165752229676,0.933469726429385,
0.993085946739478)) ;
#85778=CARTESIAN_POINT('Ctrl Pts',(-1.44851666244568,0.891242719575706,
0.9883504999456)) ;
#85779=CARTESIAN_POINT('Ctrl Pts',(-1.49846029218269,0.804436155272762,
0.978809572938975)) ;
#85780=CARTESIAN_POINT('Ctrl Pts',(-1.52155409277454,0.759863699489269,
0.974004380738511)) ;
#85781=CARTESIAN_POINT('Ctrl Pts',(-1.56372038771819,0.668800495388183,
0.964371574954774)) ;
#85782=CARTESIAN_POINT('Ctrl Pts',(-1.58279580340978,0.622312027589206,
0.959544056383236)) ;
#85783=CARTESIAN_POINT('Ctrl Pts',(-1.61678680590419,0.527762386483063,
0.949902364163737)) ;
#85784=CARTESIAN_POINT('Ctrl Pts',(-1.63168715416542,0.479696957243388,
0.94508837300885)) ;
#85785=CARTESIAN_POINT('Ctrl Pts',(-1.65714864240798,0.382601785396132,
0.935534330032484)) ;
#85786=CARTESIAN_POINT('Ctrl Pts',(-1.66769792412419,0.333570562993271,
0.930794582833185)) ;
#85787=CARTESIAN_POINT('Ctrl Pts',(-1.68445485092669,0.2348236408896,0.921413954693928)) ;
#85788=CARTESIAN_POINT('Ctrl Pts',(-1.69062301750293,0.185106508541409,
0.916774398011078)) ;
#85789=CARTESIAN_POINT('Ctrl Pts',(-1.69821839440309,0.0901591601298727,
0.908067833557157)) ;
#85790=CARTESIAN_POINT('Ctrl Pts',(-1.69999999999986,0.0449019172846421,
0.903985397709019)) ;
#85791=CARTESIAN_POINT('Ctrl Pts',(-1.69999999999986,-0.0491344664215853,
0.895638930322986)) ;
#85792=CARTESIAN_POINT('Ctrl Pts',(-1.69786604855668,-0.0986947229195726,
0.891161614336394)) ;
#85793=CARTESIAN_POINT('Ctrl Pts',(-1.68919704412223,-0.19762241240327,
0.882062291759915)) ;
#85794=CARTESIAN_POINT('Ctrl Pts',(-1.68270496892842,-0.246986299885236,
0.877442179927406)) ;
#85795=CARTESIAN_POINT('Ctrl Pts',(-1.66532644813145,-0.34520090095047,
0.868085946739475)) ;
#85796=CARTESIAN_POINT('Ctrl Pts',(-1.65445972537215,-0.394052183982064,
0.863350499945597)) ;
#85797=CARTESIAN_POINT('Ctrl Pts',(-1.62839369436614,-0.490749173516282,
0.853809572938973)) ;
#85798=CARTESIAN_POINT('Ctrl Pts',(-1.61320599162936,-0.538596442256787,
0.849004380738509)) ;
#85799=CARTESIAN_POINT('Ctrl Pts',(-1.57863065558508,-0.632803924485399,
0.839371574954773)) ;
#85800=CARTESIAN_POINT('Ctrl Pts',(-1.55924670054692,-0.679164591102501,
0.834544056383236)) ;
#85801=CARTESIAN_POINT('Ctrl Pts',(-1.51642527652514,-0.770056551850542,
0.824902364163736)) ;
#85802=CARTESIAN_POINT('Ctrl Pts',(-1.49297402286668,-0.814580080104112,
0.820088373008848)) ;
#85803=CARTESIAN_POINT('Ctrl Pts',(-1.44232135942842,-0.901240725533217,
0.810534330032481)) ;
#85804=CARTESIAN_POINT('Ctrl Pts',(-1.41511051821566,-0.94337050402234,
0.805794582833179)) ;
#85805=CARTESIAN_POINT('Ctrl Pts',(-1.35713483654874,-1.02504405883705,
0.796413954693922)) ;
#85806=CARTESIAN_POINT('Ctrl Pts',(-1.32634106753772,-1.06456093267515,
0.791774398011072)) ;
#85807=CARTESIAN_POINT('Ctrl Pts',(-1.26457389613203,-1.13706958910438,
0.783067833557153)) ;
#85808=CARTESIAN_POINT('Ctrl Pts',(-1.23383197821725,-1.17033107781691,
0.778985397709017)) ;
#85809=CARTESIAN_POINT('Ctrl Pts',(-1.16733821362031,-1.23682484241385,
0.770638930322983)) ;
#85810=CARTESIAN_POINT('Ctrl Pts',(-1.13078488863702,-1.27036030432474,
0.766161614336389)) ;
#85811=CARTESIAN_POINT('Ctrl Pts',(-1.05470253673422,-1.33418283258406,
0.757062291759907)) ;
#85812=CARTESIAN_POINT('Ctrl Pts',(-1.01520640675647,-1.36449778177477,
0.752442179927397)) ;
#85813=CARTESIAN_POINT('Ctrl Pts',(-0.933469726429203,-1.42165752229699,
0.74308594673947)) ;
#85814=CARTESIAN_POINT('Ctrl Pts',(-0.891242719575537,-1.4485166624459,
0.738350499945593)) ;
#85815=CARTESIAN_POINT('Ctrl Pts',(-0.804436155272612,-1.49846029218289,
0.72880957293897)) ;
#85816=CARTESIAN_POINT('Ctrl Pts',(-0.759863699489124,-1.52155409277474,
0.724004380738507)) ;
#85817=CARTESIAN_POINT('Ctrl Pts',(-0.668800495388052,-1.56372038771838,
0.714371574954771)) ;
#85818=CARTESIAN_POINT('Ctrl Pts',(-0.622312027589085,-1.58279580340996,
0.709544056383234)) ;
#85819=CARTESIAN_POINT('Ctrl Pts',(-0.527762386482951,-1.61678680590438,
0.699902364163737)) ;
#85820=CARTESIAN_POINT('Ctrl Pts',(-0.479696957243274,-1.6316871541656,
0.695088373008849)) ;
#85821=CARTESIAN_POINT('Ctrl Pts',(-0.382601785395997,-1.65714864240817,
0.685534330032481)) ;
#85822=CARTESIAN_POINT('Ctrl Pts',(-0.333570562993116,-1.66769792412438,
0.68079458283318)) ;
#85823=CARTESIAN_POINT('Ctrl Pts',(-0.234823640889432,-1.68445485092688,
0.671413954693923)) ;
#85824=CARTESIAN_POINT('Ctrl Pts',(-0.185106508541249,-1.69062301750311,
0.666774398011073)) ;
#85825=CARTESIAN_POINT('Ctrl Pts',(-0.0901591601297333,-1.69821839440327,
0.658067833557153)) ;
#85826=CARTESIAN_POINT('Ctrl Pts',(-0.0449019172845196,-1.70000000000004,
0.653985397709018)) ;
#85827=CARTESIAN_POINT('Ctrl Pts',(0.0491344664216406,-1.70000000000004,
0.645638930322991)) ;
#85828=CARTESIAN_POINT('Ctrl Pts',(0.098694722919575,-1.69786604855686,
0.641161614336403)) ;
#85829=CARTESIAN_POINT('Ctrl Pts',(0.197622412403214,-1.68919704412242,
0.63206229175993)) ;
#85830=CARTESIAN_POINT('Ctrl Pts',(0.246986299885175,-1.68270496892862,
0.627442179927422)) ;
#85831=CARTESIAN_POINT('Ctrl Pts',(0.345200900950416,-1.66532644813167,
0.618085946739491)) ;
#85832=CARTESIAN_POINT('Ctrl Pts',(0.394052183982023,-1.65445972537236,
0.613350499945611)) ;
#85833=CARTESIAN_POINT('Ctrl Pts',(0.490749173516293,-1.62839369436635,
0.603809572938982)) ;
#85834=CARTESIAN_POINT('Ctrl Pts',(0.538596442256835,-1.61320599162956,
0.599004380738515)) ;
#85835=CARTESIAN_POINT('Ctrl Pts',(0.632803924485532,-1.57863065558525,
0.58937157495477)) ;
#85836=CARTESIAN_POINT('Ctrl Pts',(0.67916459110268,-1.55924670054707,0.584544056383228)) ;
#85837=CARTESIAN_POINT('Ctrl Pts',(0.770056551850753,-1.51642527652527,
0.574902364163725)) ;
#85838=CARTESIAN_POINT('Ctrl Pts',(0.814580080104313,-1.4929740228668,0.570088373008839)) ;
#85839=CARTESIAN_POINT('Ctrl Pts',(0.901240725533383,-1.44232135942856,
0.560534330032474)) ;
#85840=CARTESIAN_POINT('Ctrl Pts',(0.943370504022482,-1.41511051821581,
0.555794582833176)) ;
#85841=CARTESIAN_POINT('Ctrl Pts',(1.02504405883715,-1.35713483654892,0.546413954693923)) ;
#85842=CARTESIAN_POINT('Ctrl Pts',(1.06456093267523,-1.32634106753792,0.541774398011074)) ;
#85843=CARTESIAN_POINT('Ctrl Pts',(1.13706958910446,-1.26457389613223,0.533067833557155)) ;
#85844=CARTESIAN_POINT('Ctrl Pts',(1.170331077817,-1.23383197821744,0.528985397709019)) ;
#85845=CARTESIAN_POINT('Ctrl Pts',(1.23682484241396,-1.16733821362048,0.520638930322983)) ;
#85846=CARTESIAN_POINT('Ctrl Pts',(1.27036030432486,-1.13078488863718,0.516161614336386)) ;
#85847=CARTESIAN_POINT('Ctrl Pts',(1.33418283258419,-1.05470253673437,0.507062291759903)) ;
#85848=CARTESIAN_POINT('Ctrl Pts',(1.36449778177489,-1.01520640675662,0.502442179927395)) ;
#85849=CARTESIAN_POINT('Ctrl Pts',(1.42165752229712,-0.933469726429342,
0.493085946739464)) ;
#85850=CARTESIAN_POINT('Ctrl Pts',(1.44851666244603,-0.891242719575662,
0.488350499945587)) ;
#85851=CARTESIAN_POINT('Ctrl Pts',(1.49846029218302,-0.804436155272731,
0.478809572938964)) ;
#85852=CARTESIAN_POINT('Ctrl Pts',(1.52155409277486,-0.75986369948925,0.474004380738501)) ;
#85853=CARTESIAN_POINT('Ctrl Pts',(1.5637203877185,-0.66880049538819,0.464371574954767)) ;
#85854=CARTESIAN_POINT('Ctrl Pts',(1.58279580341008,-0.622312027589227,
0.459544056383231)) ;
#85855=CARTESIAN_POINT('Ctrl Pts',(1.61678680590449,-0.527762386483097,
0.449902364163734)) ;
#85856=CARTESIAN_POINT('Ctrl Pts',(1.63168715416571,-0.479696957243424,
0.445088373008846)) ;
#85857=CARTESIAN_POINT('Ctrl Pts',(1.65714864240828,-0.382601785396136,
0.435534330032477)) ;
#85858=CARTESIAN_POINT('Ctrl Pts',(1.66769792412449,-0.333570562993245,
0.430794582833176)) ;
#85859=CARTESIAN_POINT('Ctrl Pts',(1.68445485092699,-0.234823640889562,
0.421413954693918)) ;
#85860=CARTESIAN_POINT('Ctrl Pts',(1.69062301750322,-0.185106508541393,
0.41677439801107)) ;
#85861=CARTESIAN_POINT('Ctrl Pts',(1.69821839440337,-0.0901591601298977,
0.408067833557153)) ;
#85862=CARTESIAN_POINT('Ctrl Pts',(1.70000000000014,-0.0449019172846905,
0.403985397709017)) ;
#85863=CARTESIAN_POINT('Ctrl Pts',(1.70000000000014,0.0491344664214081,
0.395638930322996)) ;
#85864=CARTESIAN_POINT('Ctrl Pts',(1.69786604855697,0.0986947229192886,
0.391161614336413)) ;
#85865=CARTESIAN_POINT('Ctrl Pts',(1.68919704412254,0.197622412402883,0.382062291759944)) ;
#85866=CARTESIAN_POINT('Ctrl Pts',(1.68270496892874,0.246986299884855,0.377442179927436)) ;
#85867=CARTESIAN_POINT('Ctrl Pts',(1.6653264481318,0.345200900950092,0.368085946739505)) ;
#85868=CARTESIAN_POINT('Ctrl Pts',(1.6544597253725,0.39405218398168,0.363350499945627)) ;
#85869=CARTESIAN_POINT('Ctrl Pts',(1.62839369436652,0.490749173515883,0.353809572939006)) ;
#85870=CARTESIAN_POINT('Ctrl Pts',(1.61320599162975,0.538596442256374,0.349004380738543)) ;
#85871=CARTESIAN_POINT('Ctrl Pts',(1.5786306555855,0.632803924484977,0.339371574954809)) ;
#85872=CARTESIAN_POINT('Ctrl Pts',(1.55924670054735,0.679164591102084,0.334544056383272)) ;
#85873=CARTESIAN_POINT('Ctrl Pts',(1.5164252765256,0.770056551850128,0.324902364163773)) ;
#85874=CARTESIAN_POINT('Ctrl Pts',(1.49297402286714,0.8145800801037,0.320088373008886)) ;
#85875=CARTESIAN_POINT('Ctrl Pts',(1.44232135942892,0.901240725532785,0.310534330032521)) ;
#85876=CARTESIAN_POINT('Ctrl Pts',(1.41511051821619,0.943370504021889,0.305794582833223)) ;
#85877=CARTESIAN_POINT('Ctrl Pts',(1.35713483654931,1.02504405883658,0.296413954693968)) ;
#85878=CARTESIAN_POINT('Ctrl Pts',(1.32634106753831,1.06456093267469,0.291774398011117)) ;
#85879=CARTESIAN_POINT('Ctrl Pts',(1.26457389613253,1.13706958910406,0.283067833557182)) ;
#85880=CARTESIAN_POINT('Ctrl Pts',(1.23383197821764,1.17033107781672,0.278985397709031)) ;
#85881=CARTESIAN_POINT('Ctrl Pts',(1.16687638181328,1.23728667422108,0.270580960013422)) ;
#85882=CARTESIAN_POINT('Ctrl Pts',(1.12981271916814,1.27125155805816,0.266042558666344)) ;
#85883=CARTESIAN_POINT('Ctrl Pts',(1.05312491055298,1.33542920601837,0.256876436955199)) ;
#85884=CARTESIAN_POINT('Ctrl Pts',(1.01357775753582,1.36570865657345,0.252253098649823)) ;
#85885=CARTESIAN_POINT('Ctrl Pts',(0.931748953624498,1.42278628521131,0.242891701206208)) ;
#85886=CARTESIAN_POINT('Ctrl Pts',(0.88948121648888,1.44959928904487,0.238154331961916)) ;
#85887=CARTESIAN_POINT('Ctrl Pts',(0.802605102103923,1.49944189580254,0.228610939181518)) ;
#85888=CARTESIAN_POINT('Ctrl Pts',(0.758004130384641,1.5224813065182,0.223805212363041)) ;
#85889=CARTESIAN_POINT('Ctrl Pts',(0.664522073922145,1.56562908564902,0.213921625026436)) ;
#85890=CARTESIAN_POINT('Ctrl Pts',(0.615539322328646,1.58552627802381,0.208842504663212)) ;
#85891=CARTESIAN_POINT('Ctrl Pts',(0.518395366613399,1.61981274547806,0.198959682063373)) ;
#85892=CARTESIAN_POINT('Ctrl Pts',(0.470304511490864,1.63441700888879,0.194154319763053)) ;
#85893=CARTESIAN_POINT('Ctrl Pts',(0.373202345586565,1.65928853338962,0.184621349139331)) ;
#85894=CARTESIAN_POINT('Ctrl Pts',(0.324189726756498,1.66954434240007,0.179894045756642)) ;
#85895=CARTESIAN_POINT('Ctrl Pts',(0.225636251909037,1.68570400886284,0.170552555999424)) ;
#85896=CARTESIAN_POINT('Ctrl Pts',(0.176094787103018,1.69157920510122,0.165939369337106)) ;
#85897=CARTESIAN_POINT('Ctrl Pts',(0.120082623975991,1.69576670628109,0.16081390877527)) ;
#85898=CARTESIAN_POINT('Ctrl Pts',(0.113425528473636,1.69622494453036,0.160206193633126)) ;
#85899=CARTESIAN_POINT('Ctrl Pts',(0.106818383502283,1.69664075012557,0.159604472052141)) ;
#85900=CARTESIAN_POINT('Ctrl Pts',(0.10676868707791,1.69664387765666,0.159599946131918)) ;
#85901=CARTESIAN_POINT('Origin',(1.41383259008656E-13,-3.66373598126302E-14,
0.700000000000004)) ;
#85902=CARTESIAN_POINT('Ctrl Pts',(1.4210854715202E-13,2.79999999999996,
0.250000000000004)) ;
#85903=CARTESIAN_POINT('Ctrl Pts',(-0.0714659907350962,2.79999999999996,
0.246148790980329)) ;
#85904=CARTESIAN_POINT('Ctrl Pts',(-0.143478336980131,2.79726014197784,
0.242206982029767)) ;
#85905=CARTESIAN_POINT('Ctrl Pts',(-0.215722164100012,2.79167762249077,
0.238189246611963)) ;
#85906=CARTESIAN_POINT('Ctrl Pts',(-0.287457311956658,2.78613441033296,
0.23419980065187)) ;
#85907=CARTESIAN_POINT('Ctrl Pts',(-0.359420096618108,2.77778812917788,
0.230135519136895)) ;
#85908=CARTESIAN_POINT('Ctrl Pts',(-0.431282451390436,2.76658552138233,
0.22601289236656)) ;
#85909=CARTESIAN_POINT('Ctrl Pts',(-0.5036778944852,2.75529981055716,0.221859683183557)) ;
#85910=CARTESIAN_POINT('Ctrl Pts',(-0.575970755470603,2.74111495138341,
0.217647288883837)) ;
#85911=CARTESIAN_POINT('Ctrl Pts',(-0.647814825564774,2.7240293595661,0.213394330843329)) ;
#85912=CARTESIAN_POINT('Ctrl Pts',(-0.718447061158909,2.70723196007406,
0.209213109847701)) ;
#85913=CARTESIAN_POINT('Ctrl Pts',(-0.788644831509182,2.6876309490148,0.204992721002004)) ;
#85914=CARTESIAN_POINT('Ctrl Pts',(-0.858078848059242,2.66527685063163,
0.200752037010299)) ;
#85915=CARTESIAN_POINT('Ctrl Pts',(-0.927415582479881,2.64295407197328,
0.196517294526654)) ;
#85916=CARTESIAN_POINT('Ctrl Pts',(-0.995990034367923,2.61788602769458,
0.192262352203906)) ;
#85917=CARTESIAN_POINT('Ctrl Pts',(-1.06348409699106,2.59017404346631,0.18800661413264)) ;
#85918=CARTESIAN_POINT('Ctrl Pts',(-1.13098269716956,2.56246019619026,0.183750589952547)) ;
#85919=CARTESIAN_POINT('Ctrl Pts',(-1.19740013263746,2.53210230701722,0.17949380953608)) ;
#85920=CARTESIAN_POINT('Ctrl Pts',(-1.26243781057895,2.49925004239673,0.175255704429561)) ;
#85921=CARTESIAN_POINT('Ctrl Pts',(-1.32956223361862,2.46534370720774,0.17088161899077)) ;
#85922=CARTESIAN_POINT('Ctrl Pts',(-1.39521615896152,2.42878055176483,0.166527472731199)) ;
#85923=CARTESIAN_POINT('Ctrl Pts',(-1.45910321389809,2.38977358994354,0.162213991563582)) ;
#85924=CARTESIAN_POINT('Ctrl Pts',(-1.5214394991492,2.35171346804115,0.158005214171092)) ;
#85925=CARTESIAN_POINT('Ctrl Pts',(-1.58209333573967,2.31132743945085,0.15383518418232)) ;
#85926=CARTESIAN_POINT('Ctrl Pts',(-1.64082699786767,2.2688514193459,0.149721978294324)) ;
#85927=CARTESIAN_POINT('Ctrl Pts',(-1.70175237824719,2.22479035473423,0.145455283110917)) ;
#85928=CARTESIAN_POINT('Ctrl Pts',(-1.76061095855609,2.17848089233263,0.14124977763669)) ;
#85929=CARTESIAN_POINT('Ctrl Pts',(-1.81718623839227,2.1302192786183,0.137123741440487)) ;
#85930=CARTESIAN_POINT('Ctrl Pts',(-1.87376151822845,2.08195766490396,0.132997705244284)) ;
#85931=CARTESIAN_POINT('Ctrl Pts',(-1.92805331228597,2.03174466235851,0.128951165331679)) ;
#85932=CARTESIAN_POINT('Ctrl Pts',(-1.97989898732219,1.97989898732229,0.125000000000004)) ;
#85933=CARTESIAN_POINT('Ctrl Pts',(-2.03043307399602,1.92936490064846,0.121148790980274)) ;
#85934=CARTESIAN_POINT('Ctrl Pts',(-2.0794161201688,1.87650711010172,0.117206982029653)) ;
#85935=CARTESIAN_POINT('Ctrl Pts',(-2.12655278283934,1.82147557266011,0.113189246611789)) ;
#85936=CARTESIAN_POINT('Ctrl Pts',(-2.17335754943038,1.76683152025651,0.109199800651814)) ;
#85937=CARTESIAN_POINT('Ctrl Pts',(-2.21834121045375,1.71004443522861,0.105135519136963)) ;
#85938=CARTESIAN_POINT('Ctrl Pts',(-2.26123412888485,1.6513086369197,0.101012892366755)) ;
#85939=CARTESIAN_POINT('Ctrl Pts',(-2.30444523496933,1.59213712552534,0.0968596831837452)) ;
#85940=CARTESIAN_POINT('Ctrl Pts',(-2.3455337970917,1.53098814317919,0.0926472888840185)) ;
#85941=CARTESIAN_POINT('Ctrl Pts',(-2.38425388840886,1.46810537619287,0.0883943308435033)) ;
#85942=CARTESIAN_POINT('Ctrl Pts',(-2.42232086608197,1.4062832883449,0.0842131098477466)) ;
#85943=CARTESIAN_POINT('Ctrl Pts',(-2.45809817768381,1.34278596106596,0.0799927210019183)) ;
#85944=CARTESIAN_POINT('Ctrl Pts',(-2.49138870707828,1.27788196256228,0.0757520370100814)) ;
#85945=CARTESIAN_POINT('Ctrl Pts',(-2.52463259401001,1.21306889930012,0.0715172945261934)) ;
#85946=CARTESIAN_POINT('Ctrl Pts',(-2.55539626985716,1.14685365524949,0.0672623522032017)) ;
#85947=CARTESIAN_POINT('Ctrl Pts',(-2.58352644726108,1.07953281390689,0.0630066141316928)) ;
#85948=CARTESIAN_POINT('Ctrl Pts',(-2.61165851582251,1.01220744666622,0.0587505899521033)) ;
#85949=CARTESIAN_POINT('Ctrl Pts',(-2.63715646553102,0.943776958369179,
0.0544938095361427)) ;
#85950=CARTESIAN_POINT('Ctrl Pts',(-2.65991498954313,0.87455831618191,0.0502557044301233)) ;
#85951=CARTESIAN_POINT('Ctrl Pts',(-2.68340372472091,0.80311878192931,0.0458816189912835)) ;
#85952=CARTESIAN_POINT('Ctrl Pts',(-2.70397400538756,0.730840390951851,
0.0415274727316643)) ;
#85953=CARTESIAN_POINT('Ctrl Pts',(-2.72156688794631,0.658083333958098,
0.0372139915639986)) ;
#85954=CARTESIAN_POINT('Ctrl Pts',(-2.73873272767104,0.587092353655318,
0.0330052141716357)) ;
#85955=CARTESIAN_POINT('Ctrl Pts',(-2.75306423214757,0.515646379818062,
0.0288351841829885)) ;
#85956=CARTESIAN_POINT('Ctrl Pts',(-2.76456012106818,0.444080327191637,
0.0247219782951128)) ;
#85957=CARTESIAN_POINT('Ctrl Pts',(-2.77648499310844,0.369843700003427,
0.0204552831115665)) ;
#85958=CARTESIAN_POINT('Ctrl Pts',(-2.78535855947916,0.295478663836406,
0.0162497776372025)) ;
#85959=CARTESIAN_POINT('Ctrl Pts',(-2.79123720917081,0.221347785486007,
0.0121237414408675)) ;
#85960=CARTESIAN_POINT('Ctrl Pts',(-2.79711585886245,0.147216907135608,
0.00799770524453251)) ;
#85961=CARTESIAN_POINT('Ctrl Pts',(-2.79999999999986,0.0733208567888282,
0.0039511653318002)) ;
#85962=CARTESIAN_POINT('Ctrl Pts',(-2.79999999999986,-3.530509218308E-14,
3.5527136788005E-15)) ;
#85963=CARTESIAN_POINT('Ctrl Pts',(-2.79999999999986,-0.071465990727953,
-0.00385120901927697)) ;
#85964=CARTESIAN_POINT('Ctrl Pts',(-2.7972601419783,-0.143478336965554,
-0.00779301796942602)) ;
#85965=CARTESIAN_POINT('Ctrl Pts',(-2.79167762249238,-0.215722164077992,
-0.0118107533868033)) ;
#85966=CARTESIAN_POINT('Ctrl Pts',(-2.78613441033479,-0.287457311939202,
-0.0158001993471373)) ;
#85967=CARTESIAN_POINT('Ctrl Pts',(-2.77778812917958,-0.359420096605276,
-0.0198644808623646)) ;
#85968=CARTESIAN_POINT('Ctrl Pts',(-2.76658552138353,-0.431282451382235,
-0.0239871076329595)) ;
#85969=CARTESIAN_POINT('Ctrl Pts',(-2.75529981055853,-0.503677894477359,
-0.0281403168159786)) ;
#85970=CARTESIAN_POINT('Ctrl Pts',(-2.74111495138493,-0.575970755463133,
-0.0323527111157155)) ;
#85971=CARTESIAN_POINT('Ctrl Pts',(-2.72402935956772,-0.647814825557682,
-0.0366056691562411)) ;
#85972=CARTESIAN_POINT('Ctrl Pts',(-2.7072319600783,-0.718447061141654,
-0.040786890151263)) ;
#85973=CARTESIAN_POINT('Ctrl Pts',(-2.68763094902248,-0.78864483148189,
-0.0450072789963427)) ;
#85974=CARTESIAN_POINT('Ctrl Pts',(-2.66527685064352,-0.858078848022196,
-0.0492479629874277)) ;
#85975=CARTESIAN_POINT('Ctrl Pts',(-2.64295407198129,-0.927415582458213,
-0.0534827054719884)) ;
#85976=CARTESIAN_POINT('Ctrl Pts',(-2.61788602769748,-0.995990034361363,
-0.0577376477956646)) ;
#85977=CARTESIAN_POINT('Ctrl Pts',(-2.59017404346296,-1.06348409699912,
-0.0619933858678578)) ;
#85978=CARTESIAN_POINT('Ctrl Pts',(-2.56246019619536,-1.13098269715648,
-0.0662494100466235)) ;
#85979=CARTESIAN_POINT('Ctrl Pts',(-2.53210230703243,-1.1974001326039,-0.0705061904617605)) ;
#85980=CARTESIAN_POINT('Ctrl Pts',(-2.49925004242354,-1.26243781052585,
-0.0747442955669683)) ;
#85981=CARTESIAN_POINT('Ctrl Pts',(-2.46534370723371,-1.32956223357075,
-0.0791183810060595)) ;
#85982=CARTESIAN_POINT('Ctrl Pts',(-2.42878055178955,-1.39521615891874,
-0.0834725272659328)) ;
#85983=CARTESIAN_POINT('Ctrl Pts',(-2.38977358996665,-1.45910321386024,
-0.0877860084338508)) ;
#85984=CARTESIAN_POINT('Ctrl Pts',(-2.35171346806522,-1.52143949911202,
-0.0919947858263564)) ;
#85985=CARTESIAN_POINT('Ctrl Pts',(-2.31132743947584,-1.5820933357032,-0.0961648158151461)) ;
#85986=CARTESIAN_POINT('Ctrl Pts',(-2.26885141937174,-1.64082699783198,
-0.100278021703165)) ;
#85987=CARTESIAN_POINT('Ctrl Pts',(-2.22479035475663,-1.70175237821829,
-0.104544716887014)) ;
#85988=CARTESIAN_POINT('Ctrl Pts',(-2.17848089235109,-1.76061095853362,
-0.108750222361676)) ;
#85989=CARTESIAN_POINT('Ctrl Pts',(-2.1302192786324,-1.81718623837581,-0.1128762585583)) ;
#85990=CARTESIAN_POINT('Ctrl Pts',(-2.08195766491371,-1.87376151821799,
-0.117002294754924)) ;
#85991=CARTESIAN_POINT('Ctrl Pts',(-2.0317446623635,-1.92805331228106,-0.121048834667934)) ;
#85992=CARTESIAN_POINT('Ctrl Pts',(-1.97989898732219,-1.97989898732237,
-0.124999999999997)) ;
#85993=CARTESIAN_POINT('Ctrl Pts',(-1.92936490065135,-2.03043307399321,
-0.1288512090195)) ;
#85994=CARTESIAN_POINT('Ctrl Pts',(-1.87650711010787,-2.07941612016318,
-0.132793017969882)) ;
#85995=CARTESIAN_POINT('Ctrl Pts',(-1.82147557266977,-2.12655278283116,
-0.1368107533875)) ;
#85996=CARTESIAN_POINT('Ctrl Pts',(-1.76683152026772,-2.1733575494213,-0.14080019934737)) ;
#85997=CARTESIAN_POINT('Ctrl Pts',(-1.71004443524148,-2.21834121044387,
-0.144864480862115)) ;
#85998=CARTESIAN_POINT('Ctrl Pts',(-1.6513086369343,-2.26123412887429,-0.148987107632213)) ;
#85999=CARTESIAN_POINT('Ctrl Pts',(-1.59213712553966,-2.30444523495957,
-0.153140316815256)) ;
#86000=CARTESIAN_POINT('Ctrl Pts',(-1.53098814319316,-2.34553379708271,
-0.157352711115019)) ;
#86001=CARTESIAN_POINT('Ctrl Pts',(-1.46810537620645,-2.38425388840062,
-0.161605669155572)) ;
#86002=CARTESIAN_POINT('Ctrl Pts',(-1.40628328836495,-2.42232086607022,
-0.165786890150902)) ;
#86003=CARTESIAN_POINT('Ctrl Pts',(-1.3427859610928,-2.45809817766906,-0.170007278996297)) ;
#86004=CARTESIAN_POINT('Ctrl Pts',(-1.27788196259615,-2.49138870706103,
-0.1742479629877)) ;
#86005=CARTESIAN_POINT('Ctrl Pts',(-1.21306889933907,-2.52463259399128,
-0.178482705471281)) ;
#86006=CARTESIAN_POINT('Ctrl Pts',(-1.14685365529364,-2.55539626983734,
-0.182737647793968)) ;
#86007=CARTESIAN_POINT('Ctrl Pts',(-1.07953281395635,-2.58352644724055,
-0.186993385865175)) ;
#86008=CARTESIAN_POINT('Ctrl Pts',(-1.01220744670876,-2.61165851580639,
-0.191249410045235)) ;
#86009=CARTESIAN_POINT('Ctrl Pts',(-0.943776958404474,-2.63715646551875,
-0.195506190461672)) ;
#86010=CARTESIAN_POINT('Ctrl Pts',(-0.874558316209742,-2.65991498953412,
-0.199744295568167)) ;
#86011=CARTESIAN_POINT('Ctrl Pts',(-0.803118781955034,-2.68340372471343,
-0.204118381007154)) ;
#86012=CARTESIAN_POINT('Ctrl Pts',(-0.730840390975363,-2.70397400538142,
-0.208472527266922)) ;
#86013=CARTESIAN_POINT('Ctrl Pts',(-0.658083333979333,-2.72156688794133,
-0.212786008434736)) ;
#86014=CARTESIAN_POINT('Ctrl Pts',(-0.587092353674923,-2.73873272766704,
-0.216994785827209)) ;
#86015=CARTESIAN_POINT('Ctrl Pts',(-0.515646379835979,-2.75306423214443,
-0.221164815815966)) ;
#86016=CARTESIAN_POINT('Ctrl Pts',(-0.444080327207839,-2.76456012106575,
-0.22527802170395)) ;
#86017=CARTESIAN_POINT('Ctrl Pts',(-0.369843700016937,-2.77648499310689,
-0.229544716887661)) ;
#86018=CARTESIAN_POINT('Ctrl Pts',(-0.295478663847176,-2.78535855947826,
-0.233750222362187)) ;
#86019=CARTESIAN_POINT('Ctrl Pts',(-0.221347785494045,-2.79123720917034,
-0.237876258558679)) ;
#86020=CARTESIAN_POINT('Ctrl Pts',(-0.147216907140913,-2.79711585886242,
-0.242002294755171)) ;
#86021=CARTESIAN_POINT('Ctrl Pts',(-0.0733208567914072,-2.80000000000004,
-0.246048834668055)) ;
#86022=CARTESIAN_POINT('Ctrl Pts',(1.41775480244632E-13,-2.80000000000004,
-0.249999999999996)) ;
#86023=CARTESIAN_POINT('Ctrl Pts',(0.0714659907356313,-2.80000000000004,
-0.253851209019685)) ;
#86024=CARTESIAN_POINT('Ctrl Pts',(0.143478336980926,-2.7972601419779,-0.257793017970261)) ;
#86025=CARTESIAN_POINT('Ctrl Pts',(0.215722164101068,-2.79167762249079,
-0.26181075338808)) ;
#86026=CARTESIAN_POINT('Ctrl Pts',(0.287457311966629,-2.78613441033227,
-0.26580019934867)) ;
#86027=CARTESIAN_POINT('Ctrl Pts',(0.359420096637054,-2.77778812917578,
-0.26986448086416)) ;
#86028=CARTESIAN_POINT('Ctrl Pts',(0.43128245141828,-2.7665855213781,-0.273987107635021)) ;
#86029=CARTESIAN_POINT('Ctrl Pts',(0.503677894511869,-2.75529981055238,
-0.278140316817974)) ;
#86030=CARTESIAN_POINT('Ctrl Pts',(0.575970755496058,-2.74111495137817,
-0.282352711117639)) ;
#86031=CARTESIAN_POINT('Ctrl Pts',(0.647814825588991,-2.72402935956048,
-0.286605669158088)) ;
#86032=CARTESIAN_POINT('Ctrl Pts',(0.718447061190441,-2.70723196006605,
-0.290786890154163)) ;
#86033=CARTESIAN_POINT('Ctrl Pts',(0.788644831547911,-2.6876309490038,-0.295007279000315)) ;
#86034=CARTESIAN_POINT('Ctrl Pts',(0.858078848104923,-2.66527685061709,
-0.299247962992474)) ;
#86035=CARTESIAN_POINT('Ctrl Pts',(0.927415582529159,-2.64295407195629,
-0.303482705476368)) ;
#86036=CARTESIAN_POINT('Ctrl Pts',(0.995990034420632,-2.61788602767484,
-0.307737647799362)) ;
#86037=CARTESIAN_POINT('Ctrl Pts',(1.063484097047,-2.59017404344353,-0.31199338587087)) ;
#86038=CARTESIAN_POINT('Ctrl Pts',(1.13098269720771,-2.56246019617309,-0.316249410049879)) ;
#86039=CARTESIAN_POINT('Ctrl Pts',(1.19740013265829,-2.53210230700705,-0.320506190465256)) ;
#86040=CARTESIAN_POINT('Ctrl Pts',(1.26243781058317,-2.49925004239482,-0.324744295570696)) ;
#86041=CARTESIAN_POINT('Ctrl Pts',(1.32956223362246,-2.4653437072059,-0.329118381009465)) ;
#86042=CARTESIAN_POINT('Ctrl Pts',(1.39521615896498,-2.42878055176307,-0.333472527269013)) ;
#86043=CARTESIAN_POINT('Ctrl Pts',(1.45910321390119,-2.3897735899419,-0.337786008436608)) ;
#86044=CARTESIAN_POINT('Ctrl Pts',(1.52143949914924,-2.35171346804128,-0.341994785828894)) ;
#86045=CARTESIAN_POINT('Ctrl Pts',(1.58209333573682,-2.31132743945296,-0.346164815817466)) ;
#86046=CARTESIAN_POINT('Ctrl Pts',(1.64082699786211,-2.26885141935021,-0.350278021705267)) ;
#86047=CARTESIAN_POINT('Ctrl Pts',(1.70175237824273,-2.22479035473798,-0.354544716888746)) ;
#86048=CARTESIAN_POINT('Ctrl Pts',(1.76061095855268,-2.17848089233573,-0.358750222363044)) ;
#86049=CARTESIAN_POINT('Ctrl Pts',(1.81718623838984,-2.13021927862069,-0.362876258559316)) ;
#86050=CARTESIAN_POINT('Ctrl Pts',(1.87376151822699,-2.08195766490564,-0.367002294755587)) ;
#86051=CARTESIAN_POINT('Ctrl Pts',(1.92805331228543,-2.03174466235941,-0.371048834668258)) ;
#86052=CARTESIAN_POINT('Ctrl Pts',(1.97989898732247,-1.97989898732237,-0.374999999999996)) ;
#86053=CARTESIAN_POINT('Ctrl Pts',(2.03043307398575,-1.9293649006591,-0.378851209018922)) ;
#86054=CARTESIAN_POINT('Ctrl Pts',(2.07941612014859,-1.8765071101239,-0.382793017968699)) ;
#86055=CARTESIAN_POINT('Ctrl Pts',(2.12655278281006,-1.82147557269471,-0.386810753385691)) ;
#86056=CARTESIAN_POINT('Ctrl Pts',(2.17335754939861,-1.7668315202958,-0.390800199345357)) ;
#86057=CARTESIAN_POINT('Ctrl Pts',(2.21834121041981,-1.71004443527286,-0.394864480859893)) ;
#86058=CARTESIAN_POINT('Ctrl Pts',(2.26123412884909,-1.65130863696912,-0.398987107629781)) ;
#86059=CARTESIAN_POINT('Ctrl Pts',(2.30444523493625,-1.59213712557381,-0.403140316812903)) ;
#86060=CARTESIAN_POINT('Ctrl Pts',(2.34553379706123,-1.5309881432265,-0.40735271111275)) ;
#86061=CARTESIAN_POINT('Ctrl Pts',(2.38425388838089,-1.46810537623884,-0.411605669153394)) ;
#86062=CARTESIAN_POINT('Ctrl Pts',(2.4223208660529,-1.4062832883953,-0.415786890148887)) ;
#86063=CARTESIAN_POINT('Ctrl Pts',(2.45809817765399,-1.34278596112091,-0.420007278994453)) ;
#86064=CARTESIAN_POINT('Ctrl Pts',(2.49138870704804,-1.27788196262186,-0.424247962986031)) ;
#86065=CARTESIAN_POINT('Ctrl Pts',(2.52463259397961,-1.21306889936383,-0.428482705469693)) ;
#86066=CARTESIAN_POINT('Ctrl Pts',(2.55539626982691,-1.14685365531737,-0.432737647792464)) ;
#86067=CARTESIAN_POINT('Ctrl Pts',(2.58352644723128,-1.07953281397895,-0.436993385863757)) ;
#86068=CARTESIAN_POINT('Ctrl Pts',(2.61165851579408,-1.01220744674031,-0.441249410043268)) ;
#86069=CARTESIAN_POINT('Ctrl Pts',(2.63715646550409,-0.943776958445191,
-0.445506190459158)) ;
#86070=CARTESIAN_POINT('Ctrl Pts',(2.65991498951784,-0.874558316259777,
-0.449744295565114)) ;
#86071=CARTESIAN_POINT('Ctrl Pts',(2.68340372469986,-0.803118782001304,
-0.454118381004365)) ;
#86072=CARTESIAN_POINT('Ctrl Pts',(2.70397400537026,-0.73084039101769,-0.4584725272644)) ;
#86073=CARTESIAN_POINT('Ctrl Pts',(2.72156688793222,-0.658083334017594,
-0.462786008432479)) ;
#86074=CARTESIAN_POINT('Ctrl Pts',(2.73873272766113,-0.58709235370434,-0.4669947858255)) ;
#86075=CARTESIAN_POINT('Ctrl Pts',(2.75306423214098,-0.51564637985638,-0.471164815814798)) ;
#86076=CARTESIAN_POINT('Ctrl Pts',(2.76456012106405,-0.444080327219168,
-0.47527802170331)) ;
#86077=CARTESIAN_POINT('Ctrl Pts',(2.7764849931058,-0.369843700026418,-0.479544716887134)) ;
#86078=CARTESIAN_POINT('Ctrl Pts',(2.78535855947762,-0.295478663854794,
-0.483750222361771)) ;
#86079=CARTESIAN_POINT('Ctrl Pts',(2.79123720917,-0.221347785499792,-0.48787625855837)) ;
#86080=CARTESIAN_POINT('Ctrl Pts',(2.79711585886238,-0.14721690714479,-0.492002294754969)) ;
#86081=CARTESIAN_POINT('Ctrl Pts',(2.80000000000014,-0.0733208567934236,
-0.496048834667957)) ;
#86082=CARTESIAN_POINT('Ctrl Pts',(2.80000000000014,-3.98570065840431E-14,
-0.499999999999997)) ;
#86083=CARTESIAN_POINT('Ctrl Pts',(2.80000000000014,0.0714659907286896,
-0.503851209019321)) ;
#86084=CARTESIAN_POINT('Ctrl Pts',(2.79726014197852,0.143478336967113,-0.507793017969516)) ;
#86085=CARTESIAN_POINT('Ctrl Pts',(2.79167762249248,0.215722164080371,-0.51181075338694)) ;
#86086=CARTESIAN_POINT('Ctrl Pts',(2.78613441033398,0.287457311952493,-0.515800199347882)) ;
#86087=CARTESIAN_POINT('Ctrl Pts',(2.77778812917701,0.35942009662955,-0.519864480863741)) ;
#86088=CARTESIAN_POINT('Ctrl Pts',(2.76658552137832,0.431282451417391,-0.523987107634981)) ;
#86089=CARTESIAN_POINT('Ctrl Pts',(2.75529981055261,0.503677894511009,-0.528140316817935)) ;
#86090=CARTESIAN_POINT('Ctrl Pts',(2.74111495137841,0.575970755495219,-0.532352711117601)) ;
#86091=CARTESIAN_POINT('Ctrl Pts',(2.72402935956074,0.64781482558818,-0.536605669158051)) ;
#86092=CARTESIAN_POINT('Ctrl Pts',(2.7072319600679,0.718447061182986,-0.540786890153733)) ;
#86093=CARTESIAN_POINT('Ctrl Pts',(2.68763094900779,0.788644831533882,-0.545007278999483)) ;
#86094=CARTESIAN_POINT('Ctrl Pts',(2.66527685062371,0.858078848084507,-0.549247962991238)) ;
#86095=CARTESIAN_POINT('Ctrl Pts',(2.64295407196269,0.927415582511202,-0.55348270547527)) ;
#86096=CARTESIAN_POINT('Ctrl Pts',(2.61788602768083,0.995990034405129,-0.557737647798405)) ;
#86097=CARTESIAN_POINT('Ctrl Pts',(2.59017404344894,1.06348409703389,-0.561993385870055)) ;
#86098=CARTESIAN_POINT('Ctrl Pts',(2.56246019617494,1.13098269720426,-0.566249410049665)) ;
#86099=CARTESIAN_POINT('Ctrl Pts',(2.53210230700456,1.19740013266423,-0.570506190465644)) ;
#86100=CARTESIAN_POINT('Ctrl Pts',(2.49925004238731,1.26243781059807,-0.574744295571679)) ;
#86101=CARTESIAN_POINT('Ctrl Pts',(2.46534370719862,1.32956223363589,-0.579118381010364)) ;
#86102=CARTESIAN_POINT('Ctrl Pts',(2.42878055175614,1.39521615897695,-0.583472527269825)) ;
#86103=CARTESIAN_POINT('Ctrl Pts',(2.38977358993544,1.45910321391176,-0.587786008437335)) ;
#86104=CARTESIAN_POINT('Ctrl Pts',(2.35171346803545,1.52143949915813,-0.591994785829516)) ;
#86105=CARTESIAN_POINT('Ctrl Pts',(2.31132743944791,1.58209333574409,-0.596164815817983)) ;
#86106=CARTESIAN_POINT('Ctrl Pts',(2.26885141934603,1.64082699786784,-0.600278021705682)) ;
#86107=CARTESIAN_POINT('Ctrl Pts',(2.22479035473437,1.70175237824734,-0.604544716889087)) ;
#86108=CARTESIAN_POINT('Ctrl Pts',(2.17848089233277,1.76061095855623,-0.608750222363314)) ;
#86109=CARTESIAN_POINT('Ctrl Pts',(2.13021927861845,1.8171862383924,-0.612876258559516)) ;
#86110=CARTESIAN_POINT('Ctrl Pts',(2.08195766490413,1.87376151822856,-0.617002294755718)) ;
#86111=CARTESIAN_POINT('Ctrl Pts',(2.03174466235868,1.92805331228608,-0.621048834668323)) ;
#86112=CARTESIAN_POINT('Ctrl Pts',(1.97989898732247,1.97989898732229,-0.624999999999997)) ;
#86113=CARTESIAN_POINT('Ctrl Pts',(1.92934280789448,2.03045516675028,-0.628852892711265)) ;
#86114=CARTESIAN_POINT('Ctrl Pts',(1.87646083611033,2.0794589999143,-0.632796468752567)) ;
#86115=CARTESIAN_POINT('Ctrl Pts',(1.82140324313394,2.12661473377325,-0.636816033965384)) ;
#86116=CARTESIAN_POINT('Ctrl Pts',(1.76686270451503,2.17332762085388,-0.640797850820597)) ;
#86117=CARTESIAN_POINT('Ctrl Pts',(1.71018744420271,2.21822633676819,-0.644854210151207)) ;
#86118=CARTESIAN_POINT('Ctrl Pts',(1.65157064835192,2.26104276684513,-0.64896871670484)) ;
#86119=CARTESIAN_POINT('Ctrl Pts',(1.59322015670206,2.30366467596553,-0.653064530486818)) ;
#86120=CARTESIAN_POINT('Ctrl Pts',(1.53294606340057,2.34422259843339,-0.657217933521998)) ;
#86121=CARTESIAN_POINT('Ctrl Pts',(1.47098180002052,2.38248033444321,-0.661411074170311)) ;
#86122=CARTESIAN_POINT('Ctrl Pts',(1.40920818579906,2.42062036058638,-0.665591313531771)) ;
#86123=CARTESIAN_POINT('Ctrl Pts',(1.34575523781256,2.45647383441825,-0.669811010885196)) ;
#86124=CARTESIAN_POINT('Ctrl Pts',(1.28089107539402,2.48984297757431,-0.674051302933831)) ;
#86125=CARTESIAN_POINT('Ctrl Pts',(1.21613126706714,2.52315843613023,-0.678284773159621)) ;
#86126=CARTESIAN_POINT('Ctrl Pts',(1.14996533229138,2.55399715855579,-0.682538733416948)) ;
#86127=CARTESIAN_POINT('Ctrl Pts',(1.08268935536029,2.58220521256341,-0.686793792120889)) ;
#86128=CARTESIAN_POINT('Ctrl Pts',(1.01452793048841,2.61078452484886,-0.691104853474501)) ;
#86129=CARTESIAN_POINT('Ctrl Pts',(0.945227658599892,2.63666307800147,-0.695417001006243)) ;
#86130=CARTESIAN_POINT('Ctrl Pts',(0.875117841601264,2.65973095694117,-0.699710035604307)) ;
#86131=CARTESIAN_POINT('Ctrl Pts',(0.805725192645433,2.68256286970239,-0.703959155849829)) ;
#86132=CARTESIAN_POINT('Ctrl Pts',(0.735540180656531,2.70264128788266,-0.708189513573025)) ;
#86133=CARTESIAN_POINT('Ctrl Pts',(0.66489291968411,2.71991128630217,-0.712382093349892)) ;
#86134=CARTESIAN_POINT('Ctrl Pts',(0.593150457159884,2.73744901101153,-0.716639668143048)) ;
#86135=CARTESIAN_POINT('Ctrl Pts',(0.520932013366811,2.75209047495254,-0.720858244268042)) ;
#86136=CARTESIAN_POINT('Ctrl Pts',(0.448583832441685,2.76383294453045,-0.725019102062247)) ;
#86137=CARTESIAN_POINT('Ctrl Pts',(0.376235651516553,2.77557541410835,-0.729179959856452)) ;
#86138=CARTESIAN_POINT('Ctrl Pts',(0.303758415027341,2.78441910171876,-0.733283067332032)) ;
#86139=CARTESIAN_POINT('Ctrl Pts',(0.231488339806442,2.7904145119558,-0.737311433537144)) ;
#86140=CARTESIAN_POINT('Ctrl Pts',(0.212934509996843,2.79195370810077,-0.738345632280566)) ;
#86141=CARTESIAN_POINT('Ctrl Pts',(0.194394253672223,2.79330543747825,-0.739374915040527)) ;
#86142=CARTESIAN_POINT('Ctrl Pts',(0.175873072149721,2.79447108814753,-0.740399016341689)) ;
#86143=CARTESIAN_POINT('Ctrl Pts',(1.4210854715202E-13,1.69999999999996,
0.250000000000004)) ;
#86144=CARTESIAN_POINT('Ctrl Pts',(-0.70416305603412,1.69999999999996,0.187500000000004)) ;
#86145=CARTESIAN_POINT('Ctrl Pts',(-1.20208152801699,1.20208152801709,0.125000000000004)) ;
#86146=CARTESIAN_POINT('Ctrl Pts',(-1.69999999999986,0.704163056034226,
0.0625000000000035)) ;
#86147=CARTESIAN_POINT('Ctrl Pts',(-1.69999999999986,-3.54230418100775E-14,
3.53883589099269E-15)) ;
#86148=CARTESIAN_POINT('Ctrl Pts',(-1.69999999999986,-0.704163056034298,
-0.0624999999999964)) ;
#86149=CARTESIAN_POINT('Ctrl Pts',(-1.20208152801699,-1.20208152801717,
-0.124999999999997)) ;
#86150=CARTESIAN_POINT('Ctrl Pts',(-0.70416305603412,-1.70000000000004,
-0.187499999999997)) ;
#86151=CARTESIAN_POINT('Ctrl Pts',(1.41900357196165E-13,-1.70000000000004,
-0.249999999999996)) ;
#86152=CARTESIAN_POINT('Ctrl Pts',(0.704163056034403,-1.70000000000004,
-0.312499999999996)) ;
#86153=CARTESIAN_POINT('Ctrl Pts',(1.20208152801727,-1.20208152801717,-0.374999999999996)) ;
#86154=CARTESIAN_POINT('Ctrl Pts',(1.70000000000014,-0.704163056034298,
-0.437499999999997)) ;
#86155=CARTESIAN_POINT('Ctrl Pts',(1.70000000000014,-3.58394217217876E-14,
-0.499999999999997)) ;
#86156=CARTESIAN_POINT('Ctrl Pts',(1.70000000000014,0.704163056034226,-0.562499999999996)) ;
#86157=CARTESIAN_POINT('Ctrl Pts',(1.20208152801727,1.20208152801709,-0.624999999999997)) ;
#86158=CARTESIAN_POINT('Ctrl Pts',(0.747866155279392,1.65629690075497,-0.682014275214703)) ;
#86159=CARTESIAN_POINT('Ctrl Pts',(0.106776946927047,1.6966433578112,-0.740399301632037)) ;
#86160=CARTESIAN_POINT('Ctrl Pts',(1.4210854715202E-13,2.79999999999996,
0.250000000000004)) ;
#86161=CARTESIAN_POINT('Ctrl Pts',(-1.15979797464453,2.79999999999996,0.187500000000004)) ;
#86162=CARTESIAN_POINT('Ctrl Pts',(-1.97989898732219,1.97989898732229,0.125000000000004)) ;
#86163=CARTESIAN_POINT('Ctrl Pts',(-2.79999999999986,1.15979797464463,0.0625000000000035)) ;
#86164=CARTESIAN_POINT('Ctrl Pts',(-2.79999999999986,-3.53556862361244E-14,
3.53883589099269E-15)) ;
#86165=CARTESIAN_POINT('Ctrl Pts',(-2.79999999999986,-1.15979797464471,
-0.0624999999999964)) ;
#86166=CARTESIAN_POINT('Ctrl Pts',(-1.97989898732219,-1.97989898732237,
-0.124999999999997)) ;
#86167=CARTESIAN_POINT('Ctrl Pts',(-1.15979797464453,-2.80000000000004,
-0.187499999999997)) ;
#86168=CARTESIAN_POINT('Ctrl Pts',(1.41765646048259E-13,-2.80000000000004,
-0.249999999999996)) ;
#86169=CARTESIAN_POINT('Ctrl Pts',(1.15979797464481,-2.80000000000004,-0.312499999999996)) ;
#86170=CARTESIAN_POINT('Ctrl Pts',(1.97989898732247,-1.97989898732237,-0.374999999999996)) ;
#86171=CARTESIAN_POINT('Ctrl Pts',(2.80000000000014,-1.15979797464471,-0.437499999999997)) ;
#86172=CARTESIAN_POINT('Ctrl Pts',(2.80000000000014,-3.60414884436469E-14,
-0.499999999999997)) ;
#86173=CARTESIAN_POINT('Ctrl Pts',(2.80000000000014,1.15979797464463,-0.562499999999996)) ;
#86174=CARTESIAN_POINT('Ctrl Pts',(1.97989898732247,1.97989898732229,-0.624999999999997)) ;
#86175=CARTESIAN_POINT('Ctrl Pts',(1.23177954987185,2.72801842477293,-0.682014275214703)) ;
#86176=CARTESIAN_POINT('Ctrl Pts',(0.175867912585632,2.79447141286552,-0.740399301632037)) ;
#86177=CARTESIAN_POINT('Ctrl Pts',(1.4210854715202E-13,1.69999999999996,
0.250000000000004)) ;
#86178=CARTESIAN_POINT('Ctrl Pts',(-0.70416305603412,1.69999999999996,0.187500000000004)) ;
#86179=CARTESIAN_POINT('Ctrl Pts',(-1.20208152801699,1.20208152801709,0.125000000000004)) ;
#86180=CARTESIAN_POINT('Ctrl Pts',(-1.69999999999986,0.704163056034226,
0.0625000000000035)) ;
#86181=CARTESIAN_POINT('Ctrl Pts',(-1.69999999999986,-3.54230418100775E-14,
3.53883589099269E-15)) ;
#86182=CARTESIAN_POINT('Ctrl Pts',(-1.69999999999986,-0.704163056034298,
-0.0624999999999964)) ;
#86183=CARTESIAN_POINT('Ctrl Pts',(-1.20208152801699,-1.20208152801717,
-0.124999999999997)) ;
#86184=CARTESIAN_POINT('Ctrl Pts',(-0.70416305603412,-1.70000000000004,
-0.187499999999997)) ;
#86185=CARTESIAN_POINT('Ctrl Pts',(1.41900357196165E-13,-1.70000000000004,
-0.249999999999996)) ;
#86186=CARTESIAN_POINT('Ctrl Pts',(0.704163056034403,-1.70000000000004,
-0.312499999999996)) ;
#86187=CARTESIAN_POINT('Ctrl Pts',(1.20208152801727,-1.20208152801717,-0.374999999999996)) ;
#86188=CARTESIAN_POINT('Ctrl Pts',(1.70000000000014,-0.704163056034299,
-0.437499999999997)) ;
#86189=CARTESIAN_POINT('Ctrl Pts',(1.70000000000014,-3.58394217217876E-14,
-0.499999999999997)) ;
#86190=CARTESIAN_POINT('Ctrl Pts',(1.70000000000014,0.704163056034226,-0.562499999999996)) ;
#86191=CARTESIAN_POINT('Ctrl Pts',(1.20208152801727,1.20208152801709,-0.624999999999997)) ;
#86192=CARTESIAN_POINT('Ctrl Pts',(0.747870497506527,1.65629255852784,-0.682013730167249)) ;
#86193=CARTESIAN_POINT('Ctrl Pts',(0.106787672942461,1.69664268274361,-0.740398324795293)) ;
#86194=CARTESIAN_POINT('Ctrl Pts',(1.4210854715202E-13,1.69999999999996,
1.15)) ;
#86195=CARTESIAN_POINT('Ctrl Pts',(-0.70416305603412,1.69999999999996,1.0875)) ;
#86196=CARTESIAN_POINT('Ctrl Pts',(-1.20208152801699,1.20208152801709,1.025)) ;
#86197=CARTESIAN_POINT('Ctrl Pts',(-1.69999999999986,0.704163056034226,
0.962500000000004)) ;
#86198=CARTESIAN_POINT('Ctrl Pts',(-1.69999999999986,-3.54230418100775E-14,
0.900000000000004)) ;
#86199=CARTESIAN_POINT('Ctrl Pts',(-1.69999999999986,-0.704163056034298,
0.837500000000003)) ;
#86200=CARTESIAN_POINT('Ctrl Pts',(-1.20208152801699,-1.20208152801717,
0.775000000000003)) ;
#86201=CARTESIAN_POINT('Ctrl Pts',(-0.70416305603412,-1.70000000000004,
0.712500000000004)) ;
#86202=CARTESIAN_POINT('Ctrl Pts',(1.41900357196165E-13,-1.70000000000004,
0.650000000000004)) ;
#86203=CARTESIAN_POINT('Ctrl Pts',(0.704163056034403,-1.70000000000004,
0.587500000000003)) ;
#86204=CARTESIAN_POINT('Ctrl Pts',(1.20208152801727,-1.20208152801717,0.525000000000004)) ;
#86205=CARTESIAN_POINT('Ctrl Pts',(1.70000000000014,-0.704163056034299,
0.462500000000004)) ;
#86206=CARTESIAN_POINT('Ctrl Pts',(1.70000000000014,-3.58394217217876E-14,
0.400000000000004)) ;
#86207=CARTESIAN_POINT('Ctrl Pts',(1.70000000000014,0.704163056034226,0.337500000000003)) ;
#86208=CARTESIAN_POINT('Ctrl Pts',(1.20208152801727,1.20208152801709,0.275000000000003)) ;
#86209=CARTESIAN_POINT('Ctrl Pts',(0.74786742326303,1.65629563277133,0.217985883945845)) ;
#86210=CARTESIAN_POINT('Ctrl Pts',(0.106780079053036,1.69664316069034,0.159600983615826)) ;
#86211=CARTESIAN_POINT('Ctrl Pts',(0.0547743647132352,1.6999161967754,0.154864735933285)) ;
#86212=CARTESIAN_POINT('Ctrl Pts',(0.00276865037343428,1.70318923286046,
0.150128488250745)) ;
#86213=CARTESIAN_POINT('Ctrl Pts',(1.4210854715202E-13,1.69999999999996,
0.250000000000004)) ;
#86214=CARTESIAN_POINT('Ctrl Pts',(-0.70416305603412,1.69999999999996,0.187500000000004)) ;
#86215=CARTESIAN_POINT('Ctrl Pts',(-1.20208152801699,1.20208152801709,0.125000000000004)) ;
#86216=CARTESIAN_POINT('Ctrl Pts',(-1.69999999999986,0.704163056034226,
0.0625000000000035)) ;
#86217=CARTESIAN_POINT('Ctrl Pts',(-1.69999999999986,-3.54230418100775E-14,
3.53883589099269E-15)) ;
#86218=CARTESIAN_POINT('Ctrl Pts',(-1.69999999999986,-0.704163056034298,
-0.0624999999999964)) ;
#86219=CARTESIAN_POINT('Ctrl Pts',(-1.20208152801699,-1.20208152801717,
-0.124999999999997)) ;
#86220=CARTESIAN_POINT('Ctrl Pts',(-0.70416305603412,-1.70000000000004,
-0.187499999999997)) ;
#86221=CARTESIAN_POINT('Ctrl Pts',(1.41900357196165E-13,-1.70000000000004,
-0.249999999999996)) ;
#86222=CARTESIAN_POINT('Ctrl Pts',(0.704163056034403,-1.70000000000004,
-0.312499999999996)) ;
#86223=CARTESIAN_POINT('Ctrl Pts',(1.20208152801727,-1.20208152801717,-0.374999999999996)) ;
#86224=CARTESIAN_POINT('Ctrl Pts',(1.70000000000014,-0.704163056034299,
-0.437499999999997)) ;
#86225=CARTESIAN_POINT('Ctrl Pts',(1.70000000000014,-3.58394217217876E-14,
-0.499999999999997)) ;
#86226=CARTESIAN_POINT('Ctrl Pts',(1.70000000000014,0.704163056034226,-0.562499999999996)) ;
#86227=CARTESIAN_POINT('Ctrl Pts',(1.20208152801727,1.20208152801709,-0.624999999999997)) ;
#86228=CARTESIAN_POINT('Ctrl Pts',(0.74786742326303,1.65629563277133,-0.682014116054154)) ;
#86229=CARTESIAN_POINT('Ctrl Pts',(0.106780079053036,1.69664316069034,-0.740399016384173)) ;
#86230=CARTESIAN_POINT('Ctrl Pts',(0.0547743647132352,1.6999161967754,-0.745135264066715)) ;
#86231=CARTESIAN_POINT('Ctrl Pts',(0.00276865037343428,1.70318923286046,
-0.749871511749254)) ;
#86302=UNCERTAINTY_MEASURE_WITH_UNIT(LENGTH_MEASURE(0.01),#86331,
'DISTANCE_ACCURACY_VALUE',
'Maximum model space distance between geometric entities at asserted c
onnectivities') ;
#86304=UNCERTAINTY_MEASURE_WITH_UNIT(LENGTH_MEASURE(0.01),#86331,
'DISTANCE_ACCURACY_VALUE',
'Maximum model space distance between geometric entities at asserted c
onnectivities') ;
#86328=(
GEOMETRIC_REPRESENTATION_CONTEXT(3)
GLOBAL_UNCERTAINTY_ASSIGNED_CONTEXT((#86302))
GLOBAL_UNIT_ASSIGNED_CONTEXT((#86331,#86333,#86334))
REPRESENTATION_CONTEXT('','3D')
) ;
#86330=(
GEOMETRIC_REPRESENTATION_CONTEXT(3)
GLOBAL_UNCERTAINTY_ASSIGNED_CONTEXT((#86304))
GLOBAL_UNIT_ASSIGNED_CONTEXT((#86331,#86333,#86334))
REPRESENTATION_CONTEXT('','3D')
) ;
#86331=(
LENGTH_UNIT()
NAMED_UNIT(*)
SI_UNIT(.MILLI.,.METRE.)
) ;
#86333=(
NAMED_UNIT(*)
PLANE_ANGLE_UNIT()
SI_UNIT($,.RADIAN.)
) ;
#86334=(
NAMED_UNIT(*)
SI_UNIT($,.STERADIAN.)
SOLID_ANGLE_UNIT()
) ;
#86358=SHAPE_DEFINITION_REPRESENTATION(#86429,#86474) ;
#86429=PRODUCT_DEFINITION_SHAPE('',$,#86500) ;
#86474=SHAPE_REPRESENTATION('',(#36482),#86328) ;
#86476=PRODUCT_DEFINITION_CONTEXT('part definition',#86553,'design') ;
#86500=PRODUCT_DEFINITION('Lock_Washer','Lock_Washer',#86525,#86476) ;
#86525=PRODUCT_DEFINITION_FORMATION('',$,#86578) ;
#86553=APPLICATION_CONTEXT(
'Core Data for Automotive Mechanical Design Process') ;
#86554=PRODUCT_CONTEXT('part definition',#86553,'mechanical') ;
#86578=PRODUCT('Lock_Washer','Lock_Washer',$,(#86554)) ;
#86582=PRESENTATION_STYLE_ASSIGNMENT((#86587)) ;
#86587=SURFACE_STYLE_USAGE(.BOTH.,#86592) ;
#86592=SURFACE_SIDE_STYLE('',(#86597)) ;
#86597=SURFACE_STYLE_FILL_AREA(#86602) ;
#86602=FILL_AREA_STYLE('Opaque(203,203,203)',(#86607)) ;
#86607=FILL_AREA_STYLE_COLOUR('Opaque(203,203,203)',#86612) ;
#86612=COLOUR_RGB('Opaque(203,203,203)', 0.66274510, 0.83137255, 0.94901961) ;
ENDSEC;
END-ISO-10303-21;
